ISO-10303-21;
HEADER;
FILE_DESCRIPTION (('STEP AP214'),
    '1' );
FILE_NAME ('Servo-Bas.step',
    '2026-11-01T06:29:40',
    ( '' ),
    ( '' ),
    'SwSTEP 2.0',
    'SolidWorks 2024',
    '' );
FILE_SCHEMA (( 'AUTOMOTIVE_DESIGN' ));
ENDSEC;

DATA;
#8=FACE_OUTER_BOUND ( 'NONE', #1374, .T. ) ;
#16=ORIENTED_EDGE ( 'NONE', *, *, #4980, .F. ) ;
#29=FACE_OUTER_BOUND ( 'NONE', #7471, .T. ) ;
#64=VECTOR ( 'NONE', #17487, 1000.000000000000000 ) ;
#77=DIRECTION ( 'NONE',  ( 0.000000000000000000, 1.000000000000000000, 0.000000000000000000 ) ) ;
#79=DIRECTION ( 'NONE',  ( -0.000000000000000000, -1.000000000000000000, 0.000000000000000000 ) ) ;
#81=CIRCLE ( 'NONE', #4367, 34.00000000000000000 ) ;
#92=EDGE_CURVE ( 'NONE', #18509, #14793, #2739, .T. ) ;
#93=ORIENTED_EDGE ( 'NONE', *, *, #12996, .T. ) ;
#94=LINE ( 'NONE', #202, #3499 ) ;
#127=CARTESIAN_POINT ( 'NONE',  ( -34.99999999999998579, 3.000000000000000000, 21.00000000000000355 ) ) ;
#130=DIRECTION ( 'NONE',  ( 0.000000000000000000, -0.000000000000000000, 1.000000000000000000 ) ) ;
#142=AXIS2_PLACEMENT_3D ( 'NONE', #2894, #15492, #7757 ) ;
#160=CYLINDRICAL_SURFACE ( 'NONE', #19995, 3.000000000000002665 ) ;
#179=CARTESIAN_POINT ( 'NONE',  ( 22.99999999999995737, 3.000000000000000000, -36.99999999999999289 ) ) ;
#199=ORIENTED_EDGE ( 'NONE', *, *, #12617, .F. ) ;
#202=CARTESIAN_POINT ( 'NONE',  ( 35.00000000000003553, -20.00000000000000000, -23.50000000000000000 ) ) ;
#220=EDGE_CURVE ( 'NONE', #6682, #1451, #10317, .T. ) ;
#226=PLANE ( 'NONE',  #3633 ) ;
#253=AXIS2_PLACEMENT_3D ( 'NONE', #6385, #12984, #18824 ) ;
#267=ORIENTED_EDGE ( 'NONE', *, *, #19357, .T. ) ;
#278=CARTESIAN_POINT ( 'NONE',  ( -26.00000000000002842, 3.000000000000000000, 31.00000000000003908 ) ) ;
#284=CARTESIAN_POINT ( 'NONE',  ( 25.99999999999996092, 3.000000000000000000, -31.00000000000003197 ) ) ;
#291=ORIENTED_EDGE ( 'NONE', *, *, #15048, .F. ) ;
#307=DIRECTION ( 'NONE',  ( -0.000000000000000000, -1.000000000000000000, -0.000000000000000000 ) ) ;
#318=VECTOR ( 'NONE', #17699, 1000.000000000000000 ) ;
#322=CARTESIAN_POINT ( 'NONE',  ( 25.99999999999996092, 3.000000000000000000, 40.00000000000000711 ) ) ;
#357=ORIENTED_EDGE ( 'NONE', *, *, #6247, .F. ) ;
#367=CARTESIAN_POINT ( 'NONE',  ( 25.99999999999996092, 3.000000000000000000, -31.00000000000003197 ) ) ;
#388=ORIENTED_EDGE ( 'NONE', *, *, #1932, .F. ) ;
#389=VECTOR ( 'NONE', #583, 1000.000000000000000 ) ;
#395=FACE_OUTER_BOUND ( 'NONE', #6602, .T. ) ;
#422=EDGE_LOOP ( 'NONE', ( #19212, #2987, #6932, #2338 ) ) ;
#424=CARTESIAN_POINT ( 'NONE',  ( -26.00000000000002842, 3.000000000000000000, -39.99999999999999289 ) ) ;
#425=CARTESIAN_POINT ( 'NONE',  ( -39.99999999999997868, 3.000000000000000000, 26.00000000000000355 ) ) ;
#448=CARTESIAN_POINT ( 'NONE',  ( -23.00000000000003197, 3.000000000000000000, 37.00000000000000711 ) ) ;
#455=LINE ( 'NONE', #13070, #20140 ) ;
#490=LINE ( 'NONE', #9659, #4444 ) ;
#494=SHAPE_REPRESENTATION_RELATIONSHIP ( 'NONE' , 'NONE' ,  #10380, #14285 ) ;
#495=DIRECTION ( 'NONE',  ( -0.000000000000000000, -1.000000000000000000, 0.000000000000000000 ) ) ;
#527=EDGE_CURVE ( 'NONE', #5719, #9425, #9992, .T. ) ;
#552=DIRECTION ( 'NONE',  ( 0.000000000000000000, 0.000000000000000000, 1.000000000000000000 ) ) ;
#583=DIRECTION ( 'NONE',  ( -0.000000000000000000, -1.000000000000000000, -0.000000000000000000 ) ) ;
#607=CYLINDRICAL_SURFACE ( 'NONE', #3748, 36.50000000000000000 ) ;
#623=DIRECTION ( 'NONE',  ( 1.000000000000000000, -0.000000000000000000, 0.000000000000000000 ) ) ;
#634=FACE_OUTER_BOUND ( 'NONE', #3655, .T. ) ;
#641=CIRCLE ( 'NONE', #1256, 4.999999999999997335 ) ;
#659=DIRECTION ( 'NONE',  ( -0.000000000000000000, -1.000000000000000000, 0.000000000000000000 ) ) ;
#662=EDGE_CURVE ( 'NONE', #3606, #3463, #9152, .T. ) ;
#678=LINE ( 'NONE', #17896, #2364 ) ;
#683=CARTESIAN_POINT ( 'NONE',  ( 30.99999999999995737, 3.000000000000000000, 31.00000000000000000 ) ) ;
#684=VECTOR ( 'NONE', #4855, 1000.000000000000000 ) ;
#688=VERTEX_POINT ( 'NONE', #2759 ) ;
#690=ORIENTED_EDGE ( 'NONE', *, *, #19539, .T. ) ;
#692=ORIENTED_EDGE ( 'NONE', *, *, #15699, .T. ) ;
#696=CIRCLE ( 'NONE', #11915, 4.999999999999997335 ) ;
#698=CARTESIAN_POINT ( 'NONE',  ( -31.00000000000006750, 3.000000000000000000, 26.00000000000000355 ) ) ;
#742=CARTESIAN_POINT ( 'NONE',  ( -20.00000000000003197, 3.000000000000000000, 40.00000000000000711 ) ) ;
#743=ORIENTED_EDGE ( 'NONE', *, *, #527, .F. ) ;
#757=EDGE_CURVE ( 'NONE', #10287, #3606, #812, .T. ) ;
#787=MECHANICAL_DESIGN_GEOMETRIC_PRESENTATION_REPRESENTATION('',(#13630),#7704);
#812=CIRCLE ( 'NONE', #17588, 3.000000000000002665 ) ;
#824=ORIENTED_EDGE ( 'NONE', *, *, #16378, .T. ) ;
#845=CARTESIAN_POINT ( 'NONE',  ( -39.99999999999997868, 0.000000000000000000, 26.00000000000000355 ) ) ;
#850=ORIENTED_EDGE ( 'NONE', *, *, #6624, .T. ) ;
#868=ORIENTED_EDGE ( 'NONE', *, *, #3484, .T. ) ;
#869=EDGE_LOOP ( 'NONE', ( #267, #17312, #12229, #6451 ) ) ;
#907=ORIENTED_EDGE ( 'NONE', *, *, #8396, .F. ) ;
#908=ORIENTED_EDGE ( 'NONE', *, *, #7465, .T. ) ;
#909=ORIENTED_EDGE ( 'NONE', *, *, #4428, .F. ) ;
#910=EDGE_CURVE ( 'NONE', #10871, #16657, #3115, .T. ) ;
#920=CARTESIAN_POINT ( 'NONE',  ( -33.99999999999997158, 0.000000000000000000, -22.99999999999999645 ) ) ;
#966=LINE ( 'NONE', #2843, #15588 ) ;
#969=DIRECTION ( 'NONE',  ( -0.000000000000000000, -1.000000000000000000, 0.000000000000000000 ) ) ;
#987=CIRCLE ( 'NONE', #7596, 2.500000000000002220 ) ;
#1003=LINE ( 'NONE', #9086, #7299 ) ;
#1025=ORIENTED_EDGE ( 'NONE', *, *, #7894, .T. ) ;
#1029=VERTEX_POINT ( 'NONE', #15743 ) ;
#1049=ORIENTED_EDGE ( 'NONE', *, *, #220, .T. ) ;
#1067=DIRECTION ( 'NONE',  ( 0.000000000000000000, 0.000000000000000000, 1.000000000000000000 ) ) ;
#1124=LINE ( 'NONE', #6288, #3032 ) ;
#1148=ORIENTED_EDGE ( 'NONE', *, *, #13345, .F. ) ;
#1149=ORIENTED_EDGE ( 'NONE', *, *, #15445, .T. ) ;
#1152=ORIENTED_EDGE ( 'NONE', *, *, #4980, .T. ) ;
#1153=CIRCLE ( 'NONE', #12722, 36.50000000000000000 ) ;
#1169=FACE_OUTER_BOUND ( 'NONE', #7881, .T. ) ;
#1209=AXIS2_PLACEMENT_3D ( 'NONE', #11207, #77, #12560 ) ;
#1221=EDGE_CURVE ( 'NONE', #5719, #8487, #19218, .T. ) ;
#1225=ORIENTED_EDGE ( 'NONE', *, *, #9468, .F. ) ;
#1229=VECTOR ( 'NONE', #18980, 1000.000000000000000 ) ;
#1230=DIRECTION ( 'NONE',  ( -1.000000000000000000, -0.000000000000000000, -0.000000000000000000 ) ) ;
#1252=AXIS2_PLACEMENT_3D ( 'NONE', #12885, #18942, #9259 ) ;
#1256=AXIS2_PLACEMENT_3D ( 'NONE', #13287, #11739, #4107 ) ;
#1261=CARTESIAN_POINT ( 'NONE',  ( 35.00000000000003553, 0.000000000000000000, -23.50000000000000000 ) ) ;
#1267=DIRECTION ( 'NONE',  ( -1.000000000000000000, -0.000000000000000000, -1.156482317317870344E-15 ) ) ;
#1268=EDGE_CURVE ( 'NONE', #14439, #5719, #11587, .T. ) ;
#1282=CARTESIAN_POINT ( 'NONE',  ( 22.99999999999995737, 0.000000000000000000, -33.99999999999998579 ) ) ;
#1297=ORIENTED_EDGE ( 'NONE', *, *, #9374, .F. ) ;
#1333=DIRECTION ( 'NONE',  ( -0.000000000000000000, -1.000000000000000000, -0.000000000000000000 ) ) ;
#1338=DIRECTION ( 'NONE',  ( -0.000000000000000000, -1.000000000000000000, -0.000000000000000000 ) ) ;
#1349=AXIS2_PLACEMENT_3D ( 'NONE', #19256, #5337, #9870 ) ;
#1354=CARTESIAN_POINT ( 'NONE',  ( -23.00000000000003197, 3.000000000000000000, 37.00000000000000711 ) ) ;
#1355=AXIS2_PLACEMENT_3D ( 'NONE', #16391, #495, #16189 ) ;
#1360=CARTESIAN_POINT ( 'NONE',  ( 30.99999999999996092, 0.000000000000000000, -30.99999999999999289 ) ) ;
#1364=DIRECTION ( 'NONE',  ( -0.000000000000000000, -1.000000000000000000, -0.000000000000000000 ) ) ;
#1367=FACE_BOUND ( 'NONE', #8452, .T. ) ;
#1374=EDGE_LOOP ( 'NONE', ( #5976, #16, #6934, #8755 ) ) ;
#1402=DIRECTION ( 'NONE',  ( -1.000000000000000000, 0.000000000000000000, 0.000000000000000000 ) ) ;
#1436=VECTOR ( 'NONE', #12800, 1000.000000000000000 ) ;
#1451=VERTEX_POINT ( 'NONE', #1958 ) ;
#1468=VERTEX_POINT ( 'NONE', #9716 ) ;
#1477=FACE_OUTER_BOUND ( 'NONE', #6236, .T. ) ;
#1479=FACE_OUTER_BOUND ( 'NONE', #9785, .T. ) ;
#1503=EDGE_CURVE ( 'NONE', #11435, #11592, #8180, .T. ) ;
#1528=EDGE_CURVE ( 'NONE', #13169, #5210, #17949, .T. ) ;
#1563=EDGE_CURVE ( 'NONE', #7052, #19684, #19987, .T. ) ;
#1565=ORIENTED_EDGE ( 'NONE', *, *, #2933, .F. ) ;
#1603=FACE_OUTER_BOUND ( 'NONE', #6979, .T. ) ;
#1605=CARTESIAN_POINT ( 'NONE',  ( 30.99999999999999645, 3.000000000000000000, -25.99999999999999645 ) ) ;
#1620=CIRCLE ( 'NONE', #15157, 4.999999999999997335 ) ;
#1637=CARTESIAN_POINT ( 'NONE',  ( 20.99999999999996092, 3.000000000000000000, 35.00000000000000711 ) ) ;
#1653=EDGE_LOOP ( 'NONE', ( #9323, #1723, #4180, #15193 ) ) ;
#1654=LINE ( 'NONE', #6440, #1229 ) ;
#1656=PLANE ( 'NONE',  #11552 ) ;
#1659=PRODUCT_DEFINITION_SHAPE ( 'NONE', 'NONE',  #15789 ) ;
#1660=EDGE_LOOP ( 'NONE', ( #16302, #8956, #4461, #17809 ) ) ;
#1706=CARTESIAN_POINT ( 'NONE',  ( 0.000000000000000000, 26.00000000000000000, -36.50000000000000000 ) ) ;
#1712=FACE_BOUND ( 'NONE', #8055, .T. ) ;
#1717=ORIENTED_EDGE ( 'NONE', *, *, #16071, .T. ) ;
#1723=ORIENTED_EDGE ( 'NONE', *, *, #15034, .T. ) ;
#1732=LINE ( 'NONE', #19154, #18125 ) ;
#1734=CYLINDRICAL_SURFACE ( 'NONE', #19049, 34.00000000000000000 ) ;
#1739=CARTESIAN_POINT ( 'NONE',  ( -23.00000000000003197, 3.000000000000000000, 34.00000000000000711 ) ) ;
#1740=CARTESIAN_POINT ( 'NONE',  ( -31.00000000000003197, 3.000000000000000000, -30.99999999999999289 ) ) ;
#1764=FACE_OUTER_BOUND ( 'NONE', #9936, .T. ) ;
#1782=CIRCLE ( 'NONE', #142, 2.500000000000002220 ) ;
#1788=CARTESIAN_POINT ( 'NONE',  ( 34.00000000000002842, 0.000000000000000000, 26.00000000000000355 ) ) ;
#1803=CARTESIAN_POINT ( 'NONE',  ( -21.00000000000002842, -20.00000000000000000, -37.50000000000000000 ) ) ;
#1808=EDGE_CURVE ( 'NONE', #6649, #11502, #6836, .T. ) ;
#1851=DIRECTION ( 'NONE',  ( -0.000000000000000000, -1.000000000000000000, -0.000000000000000000 ) ) ;
#1863=DIRECTION ( 'NONE',  ( 0.000000000000000000, 0.000000000000000000, -1.000000000000000000 ) ) ;
#1889=DIRECTION ( 'NONE',  ( 0.000000000000000000, 0.000000000000000000, 1.000000000000000000 ) ) ;
#1895=DIRECTION ( 'NONE',  ( -1.000000000000000000, 0.000000000000000000, -1.156482317317870344E-15 ) ) ;
#1907=ORIENTED_EDGE ( 'NONE', *, *, #5503, .F. ) ;
#1913=( NAMED_UNIT ( * ) PLANE_ANGLE_UNIT ( ) SI_UNIT ( $, .RADIAN. ) );
#1923=AXIS2_PLACEMENT_3D ( 'NONE', #425, #623, #5191 ) ;
#1932=EDGE_CURVE ( 'NONE', #15316, #8829, #18030, .T. ) ;
#1938=DIRECTION ( 'NONE',  ( -1.000000000000000000, 0.000000000000000000, -0.000000000000000000 ) ) ;
#1956=ORIENTED_EDGE ( 'NONE', *, *, #13975, .T. ) ;
#1958=CARTESIAN_POINT ( 'NONE',  ( -26.00000000000002842, 3.000000000000000000, 34.00000000000000711 ) ) ;
#1983=AXIS2_PLACEMENT_3D ( 'NONE', #20160, #11082, #3248 ) ;
#2034=PLANE ( 'NONE',  #6507 ) ;
#2061=ORIENTED_EDGE ( 'NONE', *, *, #757, .F. ) ;
#2085=DIRECTION ( 'NONE',  ( 0.000000000000000000, 1.000000000000000000, 0.000000000000000000 ) ) ;
#2095=VECTOR ( 'NONE', #7347, 1000.000000000000000 ) ;
#2096=DIRECTION ( 'NONE',  ( -1.000000000000000000, 0.000000000000000000, 0.000000000000000000 ) ) ;
#2130=AXIS2_PLACEMENT_3D ( 'NONE', #11707, #5514, #16159 ) ;
#2135=VECTOR ( 'NONE', #8552, 1000.000000000000000 ) ;
#2143=VERTEX_POINT ( 'NONE', #7558 ) ;
#2151=DIRECTION ( 'NONE',  ( -0.000000000000000000, 1.000000000000000000, -0.000000000000000000 ) ) ;
#2189=EDGE_CURVE ( 'NONE', #13471, #4146, #16660, .T. ) ;
#2190=ORIENTED_EDGE ( 'NONE', *, *, #9848, .T. ) ;
#2196=DIRECTION ( 'NONE',  ( -0.000000000000000000, -1.000000000000000000, -0.000000000000000000 ) ) ;
#2234=ORIENTED_EDGE ( 'NONE', *, *, #13196, .F. ) ;
#2254=ORIENTED_EDGE ( 'NONE', *, *, #9130, .F. ) ;
#2266=CARTESIAN_POINT ( 'NONE',  ( 40.00000000000003553, 0.000000000000000000, 26.00000000000000355 ) ) ;
#2276=VECTOR ( 'NONE', #16885, 1000.000000000000000 ) ;
#2282=ORIENTED_EDGE ( 'NONE', *, *, #14155, .T. ) ;
#2287=VERTEX_POINT ( 'NONE', #11151 ) ;
#2311=ORIENTED_EDGE ( 'NONE', *, *, #8965, .F. ) ;
#2313=ORIENTED_EDGE ( 'NONE', *, *, #12617, .T. ) ;
#2324=FACE_OUTER_BOUND ( 'NONE', #16415, .T. ) ;
#2338=ORIENTED_EDGE ( 'NONE', *, *, #4510, .F. ) ;
#2339=ORIENTED_EDGE ( 'NONE', *, *, #7763, .T. ) ;
#2364=VECTOR ( 'NONE', #8519, 1000.000000000000000 ) ;
#2397=CARTESIAN_POINT ( 'NONE',  ( -34.99999999999998579, -20.00000000000000000, 21.00000000000000355 ) ) ;
#2408=DIRECTION ( 'NONE',  ( 0.000000000000000000, 0.000000000000000000, 1.000000000000000000 ) ) ;
#2454=ORIENTED_EDGE ( 'NONE', *, *, #14158, .T. ) ;
#2485=DIRECTION ( 'NONE',  ( -0.000000000000000000, -0.000000000000000000, 1.000000000000000000 ) ) ;
#2493=DIRECTION ( 'NONE',  ( 0.000000000000000000, 0.000000000000000000, -1.000000000000000000 ) ) ;
#2560=EDGE_CURVE ( 'NONE', #11965, #11435, #15589, .T. ) ;
#2589=ORIENTED_EDGE ( 'NONE', *, *, #14911, .F. ) ;
#2596=VECTOR ( 'NONE', #16608, 1000.000000000000000 ) ;
#2604=FACE_OUTER_BOUND ( 'NONE', #18593, .T. ) ;
#2612=ORIENTED_EDGE ( 'NONE', *, *, #12814, .T. ) ;
#2616=AXIS2_PLACEMENT_3D ( 'NONE', #9448, #15756, #18805 ) ;
#2620=VERTEX_POINT ( 'NONE', #6716 ) ;
#2631=VECTOR ( 'NONE', #15805, 1000.000000000000000 ) ;
#2646=ORIENTED_EDGE ( 'NONE', *, *, #18943, .T. ) ;
#2651=ORIENTED_EDGE ( 'NONE', *, *, #13715, .F. ) ;
#2652=VECTOR ( 'NONE', #1851, 1000.000000000000000 ) ;
#2660=CARTESIAN_POINT ( 'NONE',  ( 35.00000000000003553, -20.00000000000000000, -20.99999999999999645 ) ) ;
#2686=DIRECTION ( 'NONE',  ( 0.000000000000000000, 0.000000000000000000, -1.000000000000000000 ) ) ;
#2727=LINE ( 'NONE', #7488, #13051 ) ;
#2732=VECTOR ( 'NONE', #8929, 1000.000000000000000 ) ;
#2737=CARTESIAN_POINT ( 'NONE',  ( 37.00000000000003553, 3.000000000000000000, 20.00000000000000000 ) ) ;
#2739=CIRCLE ( 'NONE', #18194, 2.500000000000002220 ) ;
#2741=AXIS2_PLACEMENT_3D ( 'NONE', #5042, #3500, #8234 ) ;
#2759=CARTESIAN_POINT ( 'NONE',  ( 22.99999999999995737, 0.000000000000000000, -33.99999999999998579 ) ) ;
#2796=ORIENTED_EDGE ( 'NONE', *, *, #16071, .F. ) ;
#2811=VECTOR ( 'NONE', #13808, 1000.000000000000000 ) ;
#2817=EDGE_CURVE ( 'NONE', #10868, #18646, #13413, .T. ) ;
#2818=CARTESIAN_POINT ( 'NONE',  ( 0.000000000000000000, 16.00000000000000000, 0.000000000000000000 ) ) ;
#2840=DIRECTION ( 'NONE',  ( 0.000000000000000000, 0.000000000000000000, -1.000000000000000000 ) ) ;
#2841=LINE ( 'NONE', #4206, #11127 ) ;
#2843=CARTESIAN_POINT ( 'NONE',  ( -26.00000000000002842, 3.000000000000000000, 31.00000000000003908 ) ) ;
#2848=DIRECTION ( 'NONE',  ( -0.000000000000000000, -1.000000000000000000, 0.000000000000000000 ) ) ;
#2852=ORIENTED_EDGE ( 'NONE', *, *, #1268, .T. ) ;
#2882=DIRECTION ( 'NONE',  ( -0.000000000000000000, 1.000000000000000000, -0.000000000000000000 ) ) ;
#2894=CARTESIAN_POINT ( 'NONE',  ( 20.99999999999996092, 0.000000000000000000, 35.00000000000000711 ) ) ;
#2911=CARTESIAN_POINT ( 'NONE',  ( 0.000000000000000000, 16.00000000000000000, 0.000000000000000000 ) ) ;
#2933=EDGE_CURVE ( 'NONE', #6958, #1468, #10494, .T. ) ;
#2935=ADVANCED_FACE ( 'NONE', ( #16796 ), #18325, .F. ) ;
#2946=ORIENTED_EDGE ( 'NONE', *, *, #7339, .T. ) ;
#2987=ORIENTED_EDGE ( 'NONE', *, *, #18220, .T. ) ;
#2996=AXIS2_PLACEMENT_3D ( 'NONE', #8527, #19637, #9878 ) ;
#3003=VECTOR ( 'NONE', #16589, 1000.000000000000000 ) ;
#3014=VERTEX_POINT ( 'NONE', #17184 ) ;
#3027=AXIS2_PLACEMENT_3D ( 'NONE', #9970, #16386, #13390 ) ;
#3029=CARTESIAN_POINT ( 'NONE',  ( 37.00000000000003553, -20.00000000000000000, 20.00000000000000000 ) ) ;
#3032=VECTOR ( 'NONE', #8028, 1000.000000000000000 ) ;
#3049=VERTEX_POINT ( 'NONE', #15868 ) ;
#3070=CIRCLE ( 'NONE', #14594, 34.00000000000000000 ) ;
#3089=VERTEX_POINT ( 'NONE', #17998 ) ;
#3099=ADVANCED_FACE ( 'NONE', ( #2324 ), #11730, .F. ) ;
#3103=VECTOR ( 'NONE', #9244, 1000.000000000000000 ) ;
#3104=CARTESIAN_POINT ( 'NONE',  ( -39.99999999999997868, -20.00000000000000000, -19.99999999999999645 ) ) ;
#3115=CIRCLE ( 'NONE', #13976, 3.000000000000002665 ) ;
#3120=EDGE_CURVE ( 'NONE', #11214, #12937, #10268, .T. ) ;
#3150=DIRECTION ( 'NONE',  ( -0.000000000000000000, -1.000000000000000000, 0.000000000000000000 ) ) ;
#3161=ORIENTED_EDGE ( 'NONE', *, *, #18151, .T. ) ;
#3181=DIRECTION ( 'NONE',  ( -0.000000000000000000, 1.000000000000000000, -0.000000000000000000 ) ) ;
#3187=EDGE_CURVE ( 'NONE', #5210, #18534, #16882, .T. ) ;
#3195=ORIENTED_EDGE ( 'NONE', *, *, #4304, .F. ) ;
#3206=CARTESIAN_POINT ( 'NONE',  ( -20.00000000000003197, 3.000000000000000000, 40.00000000000000711 ) ) ;
#3207=EDGE_CURVE ( 'NONE', #12943, #11965, #678, .T. ) ;
#3244=EDGE_CURVE ( 'NONE', #10515, #9428, #16684, .T. ) ;
#3248=DIRECTION ( 'NONE',  ( 0.000000000000000000, 0.000000000000000000, -1.000000000000000000 ) ) ;
#3259=DIRECTION ( 'NONE',  ( 0.000000000000000000, 0.000000000000000000, -1.000000000000000000 ) ) ;
#3298=CARTESIAN_POINT ( 'NONE',  ( -36.99999999999997868, -20.00000000000000000, -22.99999999999999645 ) ) ;
#3305=DIRECTION ( 'NONE',  ( -0.000000000000000000, -1.000000000000000000, -0.000000000000000000 ) ) ;
#3309=DIRECTION ( 'NONE',  ( -0.000000000000000000, -1.000000000000000000, -0.000000000000000000 ) ) ;
#3311=AXIS2_PLACEMENT_3D ( 'NONE', #8558, #3928, #19374 ) ;
#3312=ORIENTED_EDGE ( 'NONE', *, *, #14897, .T. ) ;
#3351=PLANE ( 'NONE',  #12256 ) ;
#3354=LINE ( 'NONE', #12748, #20244 ) ;
#3359=DIRECTION ( 'NONE',  ( -0.000000000000000000, 1.000000000000000000, -0.000000000000000000 ) ) ;
#3388=CARTESIAN_POINT ( 'NONE',  ( 30.99999999999995737, 0.000000000000000000, 31.00000000000000000 ) ) ;
#3394=ORIENTED_EDGE ( 'NONE', *, *, #3207, .F. ) ;
#3395=AXIS2_PLACEMENT_3D ( 'NONE', #8837, #13575, #17072 ) ;
#3402=EDGE_LOOP ( 'NONE', ( #7232, #2254 ) ) ;
#3405=CARTESIAN_POINT ( 'NONE',  ( 0.000000000000000000, 50.00000000000000000, 0.000000000000000000 ) ) ;
#3408=CARTESIAN_POINT ( 'NONE',  ( 25.99999999999996092, 3.000000000000000000, -33.99999999999998579 ) ) ;
#3412=CARTESIAN_POINT ( 'NONE',  ( 22.99999999999995737, 3.000000000000000000, -33.99999999999998579 ) ) ;
#3430=FACE_OUTER_BOUND ( 'NONE', #19624, .T. ) ;
#3439=DIRECTION ( 'NONE',  ( 0.000000000000000000, 0.000000000000000000, -1.000000000000000000 ) ) ;
#3443=DIRECTION ( 'NONE',  ( 0.000000000000000000, 0.000000000000000000, 1.000000000000000000 ) ) ;
#3454=CIRCLE ( 'NONE', #14975, 2.500000000000002220 ) ;
#3455=VECTOR ( 'NONE', #16116, 1000.000000000000000 ) ;
#3463=VERTEX_POINT ( 'NONE', #13525 ) ;
#3484=EDGE_CURVE ( 'NONE', #14793, #18509, #20148, .T. ) ;
#3498=FACE_BOUND ( 'NONE', #13047, .T. ) ;
#3499=VECTOR ( 'NONE', #9793, 1000.000000000000000 ) ;
#3500=DIRECTION ( 'NONE',  ( 0.000000000000000000, 0.000000000000000000, 1.000000000000000000 ) ) ;
#3511=ADVANCED_FACE ( 'NONE', ( #18658 ), #18849, .F. ) ;
#3531=ORIENTED_EDGE ( 'NONE', *, *, #4472, .F. ) ;
#3549=ORIENTED_EDGE ( 'NONE', *, *, #2189, .T. ) ;
#3565=VECTOR ( 'NONE', #6283, 1000.000000000000000 ) ;
#3568=CARTESIAN_POINT ( 'NONE',  ( 0.000000000000000000, 50.00000000000000000, 0.000000000000000000 ) ) ;
#3571=DIRECTION ( 'NONE',  ( -0.000000000000000000, -1.000000000000000000, -0.000000000000000000 ) ) ;
#3606=VERTEX_POINT ( 'NONE', #15381 ) ;
#3633=AXIS2_PLACEMENT_3D ( 'NONE', #322, #17946, #16422 ) ;
#3655=EDGE_LOOP ( 'NONE', ( #6547, #16380, #11267, #4807 ) ) ;
#3704=ADVANCED_FACE ( 'NONE', ( #14337 ), #2034, .F. ) ;
#3707=ORIENTED_EDGE ( 'NONE', *, *, #7763, .F. ) ;
#3712=AXIS2_PLACEMENT_3D ( 'NONE', #1740, #3305, #12585 ) ;
#3716=DIRECTION ( 'NONE',  ( -0.000000000000000000, -1.000000000000000000, -0.000000000000000000 ) ) ;
#3719=AXIS2_PLACEMENT_3D ( 'NONE', #12537, #12338, #7592 ) ;
#3728=ORIENTED_EDGE ( 'NONE', *, *, #9001, .F. ) ;
#3748=AXIS2_PLACEMENT_3D ( 'NONE', #6925, #3716, #9999 ) ;
#3757=FACE_OUTER_BOUND ( 'NONE', #13643, .T. ) ;
#3765=VECTOR ( 'NONE', #2686, 1000.000000000000000 ) ;
#3775=AXIS2_PLACEMENT_3D ( 'NONE', #7519, #7719, #7819 ) ;
#3781=EDGE_CURVE ( 'NONE', #10287, #688, #17505, .T. ) ;
#3782=ORIENTED_EDGE ( 'NONE', *, *, #7636, .T. ) ;
#3791=ADVANCED_FACE ( 'NONE', ( #12905 ), #17725, .F. ) ;
#3793=EDGE_LOOP ( 'NONE', ( #5869, #12117, #19031, #12665 ) ) ;
#3803=CARTESIAN_POINT ( 'NONE',  ( 22.99999999999995737, 3.000000000000000000, -33.99999999999998579 ) ) ;
#3824=LINE ( 'NONE', #14336, #7037 ) ;
#3887=DIRECTION ( 'NONE',  ( -0.000000000000000000, -1.000000000000000000, 0.000000000000000000 ) ) ;
#3916=DIRECTION ( 'NONE',  ( -0.000000000000000000, -1.000000000000000000, -0.000000000000000000 ) ) ;
#3923=UNCERTAINTY_MEASURE_WITH_UNIT (LENGTH_MEASURE( 1.000000000000000082E-05 ), #15280, 'distance_accuracy_value', 'NONE');
#3928=DIRECTION ( 'NONE',  ( 0.000000000000000000, 1.000000000000000000, 0.000000000000000000 ) ) ;
#3937=CIRCLE ( 'NONE', #13168, 4.999999999999997335 ) ;
#3938=ADVANCED_FACE ( 'NONE', ( #8542 ), #11759, .F. ) ;
#3973=ORIENTED_EDGE ( 'NONE', *, *, #20054, .T. ) ;
#3989=DIRECTION ( 'NONE',  ( -0.000000000000000000, -1.000000000000000000, 0.000000000000000000 ) ) ;
#4031=CARTESIAN_POINT ( 'NONE',  ( 19.99999999999995381, 0.000000000000000000, -36.99999999999999289 ) ) ;
#4034=VECTOR ( 'NONE', #6878, 1000.000000000000000 ) ;
#4039=LINE ( 'NONE', #10323, #11296 ) ;
#4042=DIRECTION ( 'NONE',  ( -0.000000000000000000, -0.000000000000000000, 1.000000000000000000 ) ) ;
#4052=ORIENTED_EDGE ( 'NONE', *, *, #13580, .T. ) ;
#4062=DIRECTION ( 'NONE',  ( 0.000000000000000000, 0.000000000000000000, 1.000000000000000000 ) ) ;
#4078=EDGE_CURVE ( 'NONE', #18534, #8487, #15772, .T. ) ;
#4090=EDGE_CURVE ( 'NONE', #9868, #2143, #15745, .T. ) ;
#4107=DIRECTION ( 'NONE',  ( 0.000000000000000000, 0.000000000000000000, -1.000000000000000000 ) ) ;
#4112=ADVANCED_FACE ( 'NONE', ( #17392 ), #18501, .F. ) ;
#4120=ADVANCED_FACE ( 'NONE', ( #4839, #1603, #11112, #1712, #3498, #4933 ), #17485, .T. ) ;
#4146=VERTEX_POINT ( 'NONE', #11425 ) ;
#4161=CARTESIAN_POINT ( 'NONE',  ( 34.00000000000002842, 0.000000000000000000, 31.00000000000000000 ) ) ;
#4166=DIRECTION ( 'NONE',  ( 1.000000000000000000, 0.000000000000000000, 0.000000000000000000 ) ) ;
#4180=ORIENTED_EDGE ( 'NONE', *, *, #7724, .T. ) ;
#4196=EDGE_LOOP ( 'NONE', ( #12377, #2646 ) ) ;
#4206=CARTESIAN_POINT ( 'NONE',  ( -21.00000000000002842, -20.00000000000000000, -32.49999999999999289 ) ) ;
#4211=CARTESIAN_POINT ( 'NONE',  ( 25.99999999999996092, 0.000000000000000000, 40.00000000000000711 ) ) ;
#4227=FACE_OUTER_BOUND ( 'NONE', #1660, .T. ) ;
#4276=CIRCLE ( 'NONE', #2616, 2.500000000000002220 ) ;
#4281=ORIENTED_EDGE ( 'NONE', *, *, #10646, .T. ) ;
#4296=LINE ( 'NONE', #18305, #17708 ) ;
#4300=CARTESIAN_POINT ( 'NONE',  ( 30.99999999999995737, 3.000000000000000000, 31.00000000000000000 ) ) ;
#4304=EDGE_CURVE ( 'NONE', #18104, #10793, #18021, .T. ) ;
#4307=EDGE_LOOP ( 'NONE', ( #14630, #16766, #13754, #2454 ) ) ;
#4325=CARTESIAN_POINT ( 'NONE',  ( 30.99999999999999645, 0.000000000000000000, -25.99999999999999645 ) ) ;
#4345=LINE ( 'NONE', #4161, #3765 ) ;
#4354=VERTEX_POINT ( 'NONE', #13483 ) ;
#4361=AXIS2_PLACEMENT_3D ( 'NONE', #18254, #15276, #19990 ) ;
#4367=AXIS2_PLACEMENT_3D ( 'NONE', #5290, #6944, #13228 ) ;
#4375=ORIENTED_EDGE ( 'NONE', *, *, #6975, .T. ) ;
#4396=DIRECTION ( 'NONE',  ( -0.000000000000000000, -1.000000000000000000, 0.000000000000000000 ) ) ;
#4428=EDGE_CURVE ( 'NONE', #4146, #3049, #10577, .T. ) ;
#4441=CARTESIAN_POINT ( 'NONE',  ( -34.99999999999998579, -20.00000000000000000, 18.50000000000000355 ) ) ;
#4444=VECTOR ( 'NONE', #3181, 1000.000000000000000 ) ;
#4459=ADVANCED_FACE ( 'NONE', ( #7693 ), #9133, .F. ) ;
#4461=ORIENTED_EDGE ( 'NONE', *, *, #15018, .F. ) ;
#4472=EDGE_CURVE ( 'NONE', #3089, #12943, #4296, .T. ) ;
#4479=ORIENTED_EDGE ( 'NONE', *, *, #7241, .F. ) ;
#4510=EDGE_CURVE ( 'NONE', #14656, #2143, #2841, .T. ) ;
#4539=ORIENTED_EDGE ( 'NONE', *, *, #16339, .F. ) ;
#4560=ORIENTED_EDGE ( 'NONE', *, *, #3244, .F. ) ;
#4563=LINE ( 'NONE', #14241, #2631 ) ;
#4589=ADVANCED_FACE ( 'NONE', ( #12752 ), #160, .F. ) ;
#4593=APPLICATION_CONTEXT ( 'automotive_design' ) ;
#4606=CARTESIAN_POINT ( 'NONE',  ( -21.00000000000002842, 0.000000000000000000, -37.50000000000000000 ) ) ;
#4651=DIRECTION ( 'NONE',  ( 1.000000000000000000, -0.000000000000000000, -0.000000000000000000 ) ) ;
#4657=ORIENTED_EDGE ( 'NONE', *, *, #10607, .F. ) ;
#4712=ORIENTED_EDGE ( 'NONE', *, *, #8240, .F. ) ;
#4727=DIRECTION ( 'NONE',  ( 0.000000000000000000, -1.000000000000000000, 0.000000000000000000 ) ) ;
#4740=EDGE_CURVE ( 'NONE', #12937, #17794, #6213, .T. ) ;
#4746=ORIENTED_EDGE ( 'NONE', *, *, #220, .F. ) ;
#4766=EDGE_CURVE ( 'NONE', #688, #7437, #14099, .T. ) ;
#4807=ORIENTED_EDGE ( 'NONE', *, *, #10295, .T. ) ;
#4826=ORIENTED_EDGE ( 'NONE', *, *, #3781, .T. ) ;
#4839=FACE_BOUND ( 'NONE', #10586, .T. ) ;
#4855=DIRECTION ( 'NONE',  ( 0.000000000000000000, 0.000000000000000000, 1.000000000000000000 ) ) ;
#4870=ORIENTED_EDGE ( 'NONE', *, *, #15566, .F. ) ;
#4875=ORIENTED_EDGE ( 'NONE', *, *, #910, .T. ) ;
#4933=FACE_BOUND ( 'NONE', #17937, .T. ) ;
#4935=LINE ( 'NONE', #18351, #7331 ) ;
#4980=EDGE_CURVE ( 'NONE', #6211, #2287, #1654, .T. ) ;
#5000=CARTESIAN_POINT ( 'NONE',  ( 20.99999999999996092, 0.000000000000000000, 35.00000000000000711 ) ) ;
#5015=CARTESIAN_POINT ( 'NONE',  ( 40.00000000000003553, 3.000000000000000000, 20.00000000000000355 ) ) ;
#5020=LINE ( 'NONE', #17467, #10964 ) ;
#5029=FACE_OUTER_BOUND ( 'NONE', #9601, .T. ) ;
#5042=CARTESIAN_POINT ( 'NONE',  ( 0.000000000000000000, 0.000000000000000000, 0.000000000000000000 ) ) ;
#5054=VERTEX_POINT ( 'NONE', #5500 ) ;
#5060=DIRECTION ( 'NONE',  ( 1.000000000000000000, 0.000000000000000000, 0.000000000000000000 ) ) ;
#5063=DIRECTION ( 'NONE',  ( 0.000000000000000000, 0.000000000000000000, 1.000000000000000000 ) ) ;
#5088=ADVANCED_FACE ( 'NONE', ( #14557 ), #19390, .F. ) ;
#5089=CIRCLE ( 'NONE', #6074, 36.50000000000000000 ) ;
#5093=CARTESIAN_POINT ( 'NONE',  ( 40.00000000000003553, 0.000000000000000000, 20.00000000000000355 ) ) ;
#5094=VERTEX_POINT ( 'NONE', #17959 ) ;
#5125=CARTESIAN_POINT ( 'NONE',  ( -20.00000000000003197, 3.000000000000000000, 37.00000000000000711 ) ) ;
#5140=EDGE_CURVE ( 'NONE', #17794, #7206, #13625, .T. ) ;
#5144=DIRECTION ( 'NONE',  ( 0.000000000000000000, 0.000000000000000000, -1.000000000000000000 ) ) ;
#5191=DIRECTION ( 'NONE',  ( 0.000000000000000000, 0.000000000000000000, -1.000000000000000000 ) ) ;
#5210=VERTEX_POINT ( 'NONE', #17612 ) ;
#5219=DIRECTION ( 'NONE',  ( 0.000000000000000000, 0.000000000000000000, 1.000000000000000000 ) ) ;
#5240=DIRECTION ( 'NONE',  ( -0.000000000000000000, -1.000000000000000000, -0.000000000000000000 ) ) ;
#5290=CARTESIAN_POINT ( 'NONE',  ( 0.000000000000000000, 0.000000000000000000, 0.000000000000000000 ) ) ;
#5293=DIRECTION ( 'NONE',  ( 0.000000000000000000, 0.000000000000000000, -1.000000000000000000 ) ) ;
#5298=AXIS2_PLACEMENT_3D ( 'NONE', #20172, #9462, #14203 ) ;
#5333=ORIENTED_EDGE ( 'NONE', *, *, #2933, .T. ) ;
#5337=DIRECTION ( 'NONE',  ( 0.000000000000000000, 0.000000000000000000, 1.000000000000000000 ) ) ;
#5346=FACE_OUTER_BOUND ( 'NONE', #5456, .T. ) ;
#5356=CARTESIAN_POINT ( 'NONE',  ( 4.469960816887838430E-15, 50.00000000000000000, 36.50000000000000000 ) ) ;
#5372=CARTESIAN_POINT ( 'NONE',  ( 20.99999999999996092, 0.000000000000000000, 37.50000000000001421 ) ) ;
#5378=ORIENTED_EDGE ( 'NONE', *, *, #13284, .F. ) ;
#5381=ORIENTED_EDGE ( 'NONE', *, *, #13828, .T. ) ;
#5387=VERTEX_POINT ( 'NONE', #19635 ) ;
#5389=DIRECTION ( 'NONE',  ( 1.000000000000000000, -0.000000000000000000, -0.000000000000000000 ) ) ;
#5403=EDGE_CURVE ( 'NONE', #4354, #2287, #641, .T. ) ;
#5419=EDGE_CURVE ( 'NONE', #10868, #13471, #6906, .T. ) ;
#5441=DIRECTION ( 'NONE',  ( 0.000000000000000000, 0.000000000000000000, 1.000000000000000000 ) ) ;
#5448=DIRECTION ( 'NONE',  ( -0.000000000000000000, -1.000000000000000000, -0.000000000000000000 ) ) ;
#5456=EDGE_LOOP ( 'NONE', ( #18358, #5333, #18689, #14095 ) ) ;
#5466=CARTESIAN_POINT ( 'NONE',  ( 19.99999999999995381, 3.000000000000000000, -39.99999999999999289 ) ) ;
#5500=CARTESIAN_POINT ( 'NONE',  ( -34.99999999999998579, 3.000000000000000000, 23.50000000000000711 ) ) ;
#5503=EDGE_CURVE ( 'NONE', #11214, #3014, #13800, .T. ) ;
#5507=ORIENTED_EDGE ( 'NONE', *, *, #16689, .F. ) ;
#5514=DIRECTION ( 'NONE',  ( 1.000000000000000000, 0.000000000000000000, 0.000000000000000000 ) ) ;
#5550=PRODUCT_DEFINITION_CONTEXT ( 'detailed design', #4593, 'design' ) ;
#5604=CARTESIAN_POINT ( 'NONE',  ( -20.00000000000003197, 0.000000000000000000, 40.00000000000000711 ) ) ;
#5647=EDGE_LOOP ( 'NONE', ( #15209, #9934, #1907, #7459 ) ) ;
#5648=ADVANCED_FACE ( 'NONE', ( #2604 ), #16542, .F. ) ;
#5674=ORIENTED_EDGE ( 'NONE', *, *, #3244, .T. ) ;
#5719=VERTEX_POINT ( 'NONE', #742 ) ;
#5759=CARTESIAN_POINT ( 'NONE',  ( 37.00000000000003553, 3.000000000000000000, 20.00000000000000000 ) ) ;
#5779=CARTESIAN_POINT ( 'NONE',  ( 4.469960816887838430E-15, 3.000000000000000000, 36.50000000000000000 ) ) ;
#5808=SURFACE_STYLE_FILL_AREA ( #15174 ) ;
#5840=ORIENTED_EDGE ( 'NONE', *, *, #3187, .F. ) ;
#5863=ORIENTED_EDGE ( 'NONE', *, *, #2817, .T. ) ;
#5869=ORIENTED_EDGE ( 'NONE', *, *, #10895, .T. ) ;
#5871=DIRECTION ( 'NONE',  ( -1.000000000000000000, -0.000000000000000000, -0.000000000000000000 ) ) ;
#5886=ORIENTED_EDGE ( 'NONE', *, *, #15648, .F. ) ;
#5895=PLANE ( 'NONE',  #12313 ) ;
#5896=FACE_OUTER_BOUND ( 'NONE', #18784, .T. ) ;
#5914=DIRECTION ( 'NONE',  ( 0.000000000000000000, 0.000000000000000000, -1.000000000000000000 ) ) ;
#5931=CIRCLE ( 'NONE', #15823, 2.999999999999995559 ) ;
#5942=PLANE ( 'NONE',  #3395 ) ;
#5976=ORIENTED_EDGE ( 'NONE', *, *, #5403, .T. ) ;
#6008=EDGE_CURVE ( 'NONE', #9425, #11214, #4563, .T. ) ;
#6011=DIRECTION ( 'NONE',  ( 0.000000000000000000, 0.000000000000000000, 1.000000000000000000 ) ) ;
#6021=LINE ( 'NONE', #12194, #13018 ) ;
#6026=CIRCLE ( 'NONE', #8343, 4.999999999999997335 ) ;
#6029=ORIENTED_EDGE ( 'NONE', *, *, #7653, .F. ) ;
#6074=AXIS2_PLACEMENT_3D ( 'NONE', #3568, #14382, #5219 ) ;
#6089=ADVANCED_FACE ( 'NONE', ( #14659 ), #226, .F. ) ;
#6102=LINE ( 'NONE', #4441, #17473 ) ;
#6110=CYLINDRICAL_SURFACE ( 'NONE', #3712, 4.999999999999997335 ) ;
#6126=ORIENTED_EDGE ( 'NONE', *, *, #3484, .F. ) ;
#6132=CIRCLE ( 'NONE', #14025, 2.500000000000002220 ) ;
#6156=CARTESIAN_POINT ( 'NONE',  ( -26.00000000000002842, 3.000000000000000000, -31.00000000000003197 ) ) ;
#6163=LINE ( 'NONE', #1803, #17507 ) ;
#6164=LINE ( 'NONE', #18398, #2732 ) ;
#6165=CIRCLE ( 'NONE', #11750, 2.500000000000002220 ) ;
#6172=ADVANCED_FACE ( 'NONE', ( #3430 ), #14547, .F. ) ;
#6174=EDGE_LOOP ( 'NONE', ( #7902, #11259, #16273, #9835 ) ) ;
#6192=CARTESIAN_POINT ( 'NONE',  ( 0.000000000000000000, 50.00000000000000000, 0.000000000000000000 ) ) ;
#6196=ORIENTED_EDGE ( 'NONE', *, *, #11771, .T. ) ;
#6203=LINE ( 'NONE', #9479, #684 ) ;
#6211=VERTEX_POINT ( 'NONE', #18035 ) ;
#6213=CIRCLE ( 'NONE', #6870, 4.999999999999997335 ) ;
#6226=CARTESIAN_POINT ( 'NONE',  ( 20.99999999999996092, 3.000000000000000000, 37.50000000000001421 ) ) ;
#6236=EDGE_LOOP ( 'NONE', ( #3312, #10361, #4560, #7210 ) ) ;
#6245=DIRECTION ( 'NONE',  ( -0.000000000000000000, 1.000000000000000000, -0.000000000000000000 ) ) ;
#6247=EDGE_CURVE ( 'NONE', #15316, #13471, #7939, .T. ) ;
#6264=FACE_BOUND ( 'NONE', #17003, .T. ) ;
#6272=ORIENTED_EDGE ( 'NONE', *, *, #16378, .F. ) ;
#6283=DIRECTION ( 'NONE',  ( 0.000000000000000000, 0.000000000000000000, 1.000000000000000000 ) ) ;
#6288=CARTESIAN_POINT ( 'NONE',  ( -23.00000000000003197, 3.000000000000000000, 34.00000000000000711 ) ) ;
#6316=APPLICATION_CONTEXT ( 'automotive_design' ) ;
#6337=ORIENTED_EDGE ( 'NONE', *, *, #14822, .T. ) ;
#6365=ADVANCED_FACE ( 'NONE', ( #395 ), #6825, .F. ) ;
#6376=DIRECTION ( 'NONE',  ( 0.000000000000000000, 0.000000000000000000, 1.000000000000000000 ) ) ;
#6385=CARTESIAN_POINT ( 'NONE',  ( -21.00000000000002842, -20.00000000000000000, -34.99999999999999289 ) ) ;
#6396=ADVANCED_FACE ( 'NONE', ( #15890 ), #1734, .F. ) ;
#6404=VERTEX_POINT ( 'NONE', #3408 ) ;
#6409=CARTESIAN_POINT ( 'NONE',  ( -36.99999999999997868, -20.00000000000000000, -19.99999999999999289 ) ) ;
#6414=DIRECTION ( 'NONE',  ( -1.000000000000000000, 0.000000000000000000, -0.000000000000000000 ) ) ;
#6421=AXIS2_PLACEMENT_3D ( 'NONE', #14043, #3309, #17033 ) ;
#6426=ORIENTED_EDGE ( 'NONE', *, *, #17520, .F. ) ;
#6440=CARTESIAN_POINT ( 'NONE',  ( -31.00000000000006395, 3.000000000000000000, -25.99999999999999645 ) ) ;
#6451=ORIENTED_EDGE ( 'NONE', *, *, #18532, .F. ) ;
#6471=EDGE_CURVE ( 'NONE', #10515, #11272, #19555, .T. ) ;
#6507=AXIS2_PLACEMENT_3D ( 'NONE', #3206, #8051, #6414 ) ;
#6520=DIRECTION ( 'NONE',  ( 0.000000000000000000, 1.000000000000000000, 0.000000000000000000 ) ) ;
#6547=ORIENTED_EDGE ( 'NONE', *, *, #5140, .T. ) ;
#6554=DIRECTION ( 'NONE',  ( 0.000000000000000000, 0.000000000000000000, 1.000000000000000000 ) ) ;
#6566=DIRECTION ( 'NONE',  ( -0.000000000000000000, -1.000000000000000000, -0.000000000000000000 ) ) ;
#6591=DIRECTION ( 'NONE',  ( -0.000000000000000000, -1.000000000000000000, -0.000000000000000000 ) ) ;
#6602=EDGE_LOOP ( 'NONE', ( #7286, #17443, #3549, #18096 ) ) ;
#6624=EDGE_CURVE ( 'NONE', #16461, #9346, #9658, .T. ) ;
#6631=CYLINDRICAL_SURFACE ( 'NONE', #16938, 36.50000000000000000 ) ;
#6649=VERTEX_POINT ( 'NONE', #6688 ) ;
#6665=FACE_OUTER_BOUND ( 'NONE', #20237, .T. ) ;
#6672=DIRECTION ( 'NONE',  ( 1.156482317317870344E-15, 0.000000000000000000, -1.000000000000000000 ) ) ;
#6682=VERTEX_POINT ( 'NONE', #278 ) ;
#6683=LINE ( 'NONE', #12974, #18308 ) ;
#6688=CARTESIAN_POINT ( 'NONE',  ( -33.99999999999997158, 0.000000000000000000, -25.99999999999999645 ) ) ;
#6690=CARTESIAN_POINT ( 'NONE',  ( 30.99999999999999645, 0.000000000000000000, -25.99999999999999645 ) ) ;
#6692=AXIS2_PLACEMENT_3D ( 'NONE', #3104, #13727, #19988 ) ;
#6693=CARTESIAN_POINT ( 'NONE',  ( -20.00000000000003197, 0.000000000000000000, 37.00000000000000711 ) ) ;
#6716=CARTESIAN_POINT ( 'NONE',  ( 35.00000000000003553, 3.000000000000000000, -23.50000000000000000 ) ) ;
#6717=CIRCLE ( 'NONE', #20188, 34.00000000000000000 ) ;
#6744=ORIENTED_EDGE ( 'NONE', *, *, #18242, .T. ) ;
#6753=CARTESIAN_POINT ( 'NONE',  ( 35.00000000000003553, 0.000000000000000000, -18.49999999999999645 ) ) ;
#6795=EDGE_LOOP ( 'NONE', ( #13222, #19272, #1148, #18741 ) ) ;
#6825=CYLINDRICAL_SURFACE ( 'NONE', #18071, 3.000000000000002665 ) ;
#6827=CARTESIAN_POINT ( 'NONE',  ( 35.00000000000003553, 0.000000000000000000, -20.99999999999999645 ) ) ;
#6836=LINE ( 'NONE', #8172, #15641 ) ;
#6843=FACE_OUTER_BOUND ( 'NONE', #14493, .T. ) ;
#6863=DIRECTION ( 'NONE',  ( 0.000000000000000000, 0.000000000000000000, -1.000000000000000000 ) ) ;
#6870=AXIS2_PLACEMENT_3D ( 'NONE', #16550, #659, #16367 ) ;
#6878=DIRECTION ( 'NONE',  ( -1.000000000000000000, -0.000000000000000000, -0.000000000000000000 ) ) ;
#6906=LINE ( 'NONE', #13487, #11169 ) ;
#6925=CARTESIAN_POINT ( 'NONE',  ( 0.000000000000000000, 26.00000000000000000, 0.000000000000000000 ) ) ;
#6932=ORIENTED_EDGE ( 'NONE', *, *, #4090, .T. ) ;
#6934=ORIENTED_EDGE ( 'NONE', *, *, #13545, .F. ) ;
#6944=DIRECTION ( 'NONE',  ( 0.000000000000000000, -1.000000000000000000, 0.000000000000000000 ) ) ;
#6951=DIRECTION ( 'NONE',  ( 0.000000000000000000, 0.000000000000000000, -1.000000000000000000 ) ) ;
#6958=VERTEX_POINT ( 'NONE', #10777 ) ;
#6964=DIRECTION ( 'NONE',  ( -0.000000000000000000, -1.000000000000000000, -0.000000000000000000 ) ) ;
#6970=LINE ( 'NONE', #13254, #4034 ) ;
#6975=EDGE_CURVE ( 'NONE', #5387, #14439, #5931, .T. ) ;
#6979=EDGE_LOOP ( 'NONE', ( #3531, #14469, #2589, #12524, #18649, #6426, #3707, #8641, #5840, #7183, #12520, #9488, #4870, #4712, #388, #11922, #9119, #1297, #11432, #15575, #18317, #20238, #18672, #4657, #15007, #11009, #2796, #18290 ) ) ;
#6982=DIRECTION ( 'NONE',  ( -0.000000000000000000, 1.000000000000000000, -0.000000000000000000 ) ) ;
#6983=DIRECTION ( 'NONE',  ( 0.000000000000000000, 0.000000000000000000, 1.000000000000000000 ) ) ;
#7037=VECTOR ( 'NONE', #17631, 1000.000000000000000 ) ;
#7052=VERTEX_POINT ( 'NONE', #698 ) ;
#7066=VECTOR ( 'NONE', #4651, 1000.000000000000000 ) ;
#7078=VECTOR ( 'NONE', #10444, 1000.000000000000000 ) ;
#7100=CIRCLE ( 'NONE', #16652, 4.999999999999997335 ) ;
#7119=FACE_OUTER_BOUND ( 'NONE', #19119, .T. ) ;
#7128=DIRECTION ( 'NONE',  ( 1.000000000000000000, 0.000000000000000000, -0.000000000000000000 ) ) ;
#7148=ADVANCED_FACE ( 'NONE', ( #7119 ), #13410, .F. ) ;
#7159=ORIENTED_EDGE ( 'NONE', *, *, #5503, .T. ) ;
#7164=EDGE_LOOP ( 'NONE', ( #8889, #4539, #16266, #6744, #19285, #3973, #12623, #14680, #16813, #16967, #5674, #10021, #12357, #909, #15831, #18318, #5863, #692, #13885, #1049, #14254, #4375, #2852, #7554, #15936, #7159, #16749, #16537 ) ) ;
#7183=ORIENTED_EDGE ( 'NONE', *, *, #1528, .F. ) ;
#7185=VECTOR ( 'NONE', #9229, 1000.000000000000000 ) ;
#7206=VERTEX_POINT ( 'NONE', #1788 ) ;
#7209=ORIENTED_EDGE ( 'NONE', *, *, #11771, .F. ) ;
#7210=ORIENTED_EDGE ( 'NONE', *, *, #6471, .T. ) ;
#7232=ORIENTED_EDGE ( 'NONE', *, *, #12996, .F. ) ;
#7241=EDGE_CURVE ( 'NONE', #14656, #13534, #14832, .T. ) ;
#7243=DIRECTION ( 'NONE',  ( -0.000000000000000000, -1.000000000000000000, 0.000000000000000000 ) ) ;
#7286=ORIENTED_EDGE ( 'NONE', *, *, #8773, .T. ) ;
#7299=VECTOR ( 'NONE', #2882, 1000.000000000000000 ) ;
#7321=ORIENTED_EDGE ( 'NONE', *, *, #7339, .F. ) ;
#7331=VECTOR ( 'NONE', #11115, 1000.000000000000000 ) ;
#7339=EDGE_CURVE ( 'NONE', #11321, #11823, #987, .T. ) ;
#7343=EDGE_LOOP ( 'NONE', ( #18648, #16864, #850, #908 ) ) ;
#7344=CARTESIAN_POINT ( 'NONE',  ( 30.99999999999999645, 3.000000000000000000, 26.00000000000000355 ) ) ;
#7347=DIRECTION ( 'NONE',  ( 1.000000000000000000, 0.000000000000000000, 0.000000000000000000 ) ) ;
#7376=ORIENTED_EDGE ( 'NONE', *, *, #15699, .F. ) ;
#7398=CARTESIAN_POINT ( 'NONE',  ( -34.99999999999998579, 0.000000000000000000, 18.50000000000000355 ) ) ;
#7425=DIRECTION ( 'NONE',  ( -0.000000000000000000, 1.000000000000000000, -0.000000000000000000 ) ) ;
#7436=VECTOR ( 'NONE', #13135, 1000.000000000000000 ) ;
#7437=VERTEX_POINT ( 'NONE', #4031 ) ;
#7459=ORIENTED_EDGE ( 'NONE', *, *, #3120, .T. ) ;
#7461=CARTESIAN_POINT ( 'NONE',  ( -39.99999999999997868, 3.000000000000000000, 26.00000000000000355 ) ) ;
#7465=EDGE_CURVE ( 'NONE', #9346, #12110, #15178, .T. ) ;
#7471=EDGE_LOOP ( 'NONE', ( #1149, #14629, #5507, #8819 ) ) ;
#7477=VERTEX_POINT ( 'NONE', #10210 ) ;
#7487=ORIENTED_EDGE ( 'NONE', *, *, #14155, .F. ) ;
#7488=CARTESIAN_POINT ( 'NONE',  ( 35.00000000000003553, -20.00000000000000000, -18.49999999999999645 ) ) ;
#7500=DIRECTION ( 'NONE',  ( 0.000000000000000000, 0.000000000000000000, -1.000000000000000000 ) ) ;
#7519=CARTESIAN_POINT ( 'NONE',  ( -23.00000000000003197, 3.000000000000000000, 34.00000000000000711 ) ) ;
#7543=CARTESIAN_POINT ( 'NONE',  ( 0.000000000000000000, 0.000000000000000000, -34.00000000000000000 ) ) ;
#7554=ORIENTED_EDGE ( 'NONE', *, *, #527, .T. ) ;
#7558=CARTESIAN_POINT ( 'NONE',  ( -21.00000000000002842, 3.000000000000000000, -32.49999999999999289 ) ) ;
#7592=DIRECTION ( 'NONE',  ( 0.000000000000000000, 0.000000000000000000, -1.000000000000000000 ) ) ;
#7596=AXIS2_PLACEMENT_3D ( 'NONE', #1637, #6520, #11243 ) ;
#7616=PLANE ( 'NONE',  #14520 ) ;
#7636=EDGE_CURVE ( 'NONE', #8829, #10868, #1003, .T. ) ;
#7649=CIRCLE ( 'NONE', #14236, 2.500000000000002220 ) ;
#7653=EDGE_CURVE ( 'NONE', #18104, #18073, #6102, .T. ) ;
#7663=LINE ( 'NONE', #9196, #16290 ) ;
#7693=FACE_OUTER_BOUND ( 'NONE', #3793, .T. ) ;
#7704=( GEOMETRIC_REPRESENTATION_CONTEXT ( 3 ) GLOBAL_UNCERTAINTY_ASSIGNED_CONTEXT ( ( #3923 ) ) GLOBAL_UNIT_ASSIGNED_CONTEXT ( ( #15280, #9098, #20098 ) ) REPRESENTATION_CONTEXT ( 'NONE', 'WORKASPACE' ) );
#7719=DIRECTION ( 'NONE',  ( 0.000000000000000000, 0.000000000000000000, -1.000000000000000000 ) ) ;
#7724=EDGE_CURVE ( 'NONE', #16657, #5094, #6203, .T. ) ;
#7757=DIRECTION ( 'NONE',  ( 0.000000000000000000, 0.000000000000000000, -1.000000000000000000 ) ) ;
#7763=EDGE_CURVE ( 'NONE', #8487, #7477, #1732, .T. ) ;
#7765=EDGE_CURVE ( 'NONE', #1468, #14969, #6717, .T. ) ;
#7781=SHAPE_DEFINITION_REPRESENTATION ( #1659, #10380 ) ;
#7787=VECTOR ( 'NONE', #18520, 1000.000000000000000 ) ;
#7819=DIRECTION ( 'NONE',  ( -1.000000000000000000, 0.000000000000000000, -0.000000000000000000 ) ) ;
#7823=CARTESIAN_POINT ( 'NONE',  ( 34.00000000000002842, 3.000000000000000000, 23.00000000000000355 ) ) ;
#7837=AXIS2_PLACEMENT_3D ( 'NONE', #3388, #4727, #11310 ) ;
#7845=CARTESIAN_POINT ( 'NONE',  ( 30.99999999999999645, 3.000000000000000000, -25.99999999999999645 ) ) ;
#7881=EDGE_LOOP ( 'NONE', ( #6029, #9376, #15763, #93 ) ) ;
#7884=DIRECTION ( 'NONE',  ( 0.000000000000000000, 0.000000000000000000, 1.000000000000000000 ) ) ;
#7894=EDGE_CURVE ( 'NONE', #3463, #1029, #19554, .T. ) ;
#7902=ORIENTED_EDGE ( 'NONE', *, *, #4472, .T. ) ;
#7909=ORIENTED_EDGE ( 'NONE', *, *, #9758, .T. ) ;
#7934=CARTESIAN_POINT ( 'NONE',  ( -26.00000000000002842, 3.000000000000000000, -31.00000000000003197 ) ) ;
#7939=LINE ( 'NONE', #6409, #18053 ) ;
#7943=LINE ( 'NONE', #11761, #20090 ) ;
#7968=DIRECTION ( 'NONE',  ( 0.000000000000000000, 1.000000000000000000, 0.000000000000000000 ) ) ;
#8001=FACE_BOUND ( 'NONE', #13490, .T. ) ;
#8028=DIRECTION ( 'NONE',  ( -0.000000000000000000, -1.000000000000000000, -0.000000000000000000 ) ) ;
#8044=DIRECTION ( 'NONE',  ( 0.000000000000000000, 0.000000000000000000, -1.000000000000000000 ) ) ;
#8045=DIRECTION ( 'NONE',  ( -0.000000000000000000, -1.000000000000000000, -0.000000000000000000 ) ) ;
#8051=DIRECTION ( 'NONE',  ( 0.000000000000000000, 0.000000000000000000, -1.000000000000000000 ) ) ;
#8055=EDGE_LOOP ( 'NONE', ( #6126, #19927 ) ) ;
#8095=DIRECTION ( 'NONE',  ( 0.000000000000000000, 0.000000000000000000, -1.000000000000000000 ) ) ;
#8113=DIRECTION ( 'NONE',  ( -0.000000000000000000, 1.000000000000000000, -0.000000000000000000 ) ) ;
#8155=EDGE_CURVE ( 'NONE', #9428, #4354, #17595, .T. ) ;
#8157=CARTESIAN_POINT ( 'NONE',  ( 0.000000000000000000, 23.00000000000000000, 0.000000000000000000 ) ) ;
#8170=EDGE_LOOP ( 'NONE', ( #20007, #12572, #4875, #16651 ) ) ;
#8172=CARTESIAN_POINT ( 'NONE',  ( -33.99999999999997158, 0.000000000000000000, 31.00000000000000000 ) ) ;
#8180=LINE ( 'NONE', #11671, #12995 ) ;
#8220=CIRCLE ( 'NONE', #1252, 2.500000000000002220 ) ;
#8224=AXIS2_PLACEMENT_3D ( 'NONE', #2397, #14997, #8704 ) ;
#8234=DIRECTION ( 'NONE',  ( 1.000000000000000000, 0.000000000000000000, 0.000000000000000000 ) ) ;
#8235=LINE ( 'NONE', #3803, #18830 ) ;
#8240=EDGE_CURVE ( 'NONE', #8829, #12714, #15114, .T. ) ;
#8246=ORIENTED_EDGE ( 'NONE', *, *, #7465, .F. ) ;
#8250=ADVANCED_FACE ( 'NONE', ( #1477 ), #3351, .F. ) ;
#8283=CARTESIAN_POINT ( 'NONE',  ( 40.00000000000003553, 3.000000000000000000, -25.99999999999999645 ) ) ;
#8329=CARTESIAN_POINT ( 'NONE',  ( -26.00000000000002842, 3.000000000000000000, -31.00000000000003197 ) ) ;
#8338=LINE ( 'NONE', #19261, #17196 ) ;
#8343=AXIS2_PLACEMENT_3D ( 'NONE', #11094, #9446, #9339 ) ;
#8357=ADVANCED_FACE ( 'NONE', ( #6665 ), #19314, .F. ) ;
#8394=CARTESIAN_POINT ( 'NONE',  ( 20.99999999999996092, -20.00000000000000000, 35.00000000000000711 ) ) ;
#8396=EDGE_CURVE ( 'NONE', #6404, #19010, #455, .T. ) ;
#8420=ORIENTED_EDGE ( 'NONE', *, *, #18532, .T. ) ;
#8452=EDGE_LOOP ( 'NONE', ( #7321, #11723 ) ) ;
#8470=AXIS2_PLACEMENT_3D ( 'NONE', #19160, #16111, #1938 ) ;
#8475=ORIENTED_EDGE ( 'NONE', *, *, #1563, .F. ) ;
#8483=CARTESIAN_POINT ( 'NONE',  ( 34.00000000000002842, 0.000000000000000000, 23.00000000000000355 ) ) ;
#8487=VERTEX_POINT ( 'NONE', #5604 ) ;
#8519=DIRECTION ( 'NONE',  ( -0.000000000000000000, 1.000000000000000000, -0.000000000000000000 ) ) ;
#8520=CARTESIAN_POINT ( 'NONE',  ( -34.99999999999998579, 0.000000000000000000, 23.50000000000000711 ) ) ;
#8527=CARTESIAN_POINT ( 'NONE',  ( 0.000000000000000000, 23.00000000000000000, 0.000000000000000000 ) ) ;
#8537=ORIENTED_EDGE ( 'NONE', *, *, #13284, .T. ) ;
#8542=FACE_OUTER_BOUND ( 'NONE', #6795, .T. ) ;
#8552=DIRECTION ( 'NONE',  ( -1.000000000000000000, 0.000000000000000000, -1.156482317317870344E-15 ) ) ;
#8558=CARTESIAN_POINT ( 'NONE',  ( 0.000000000000000000, 3.000000000000000000, 0.000000000000000000 ) ) ;
#8592=CARTESIAN_POINT ( 'NONE',  ( -39.99999999999997868, 0.000000000000000000, 26.00000000000000355 ) ) ;
#8629=CARTESIAN_POINT ( 'NONE',  ( 20.99999999999996092, 0.000000000000000000, 32.50000000000000711 ) ) ;
#8637=ADVANCED_FACE ( 'NONE', ( #5029 ), #19517, .F. ) ;
#8641=ORIENTED_EDGE ( 'NONE', *, *, #4078, .F. ) ;
#8654=CIRCLE ( 'NONE', #3719, 2.500000000000002220 ) ;
#8689=AXIS2_PLACEMENT_3D ( 'NONE', #10132, #16347, #6951 ) ;
#8704=DIRECTION ( 'NONE',  ( 0.000000000000000000, 0.000000000000000000, 1.000000000000000000 ) ) ;
#8706=VECTOR ( 'NONE', #10036, 1000.000000000000000 ) ;
#8728=VECTOR ( 'NONE', #6964, 1000.000000000000000 ) ;
#8755=ORIENTED_EDGE ( 'NONE', *, *, #8155, .T. ) ;
#8773=EDGE_CURVE ( 'NONE', #11502, #15316, #11377, .T. ) ;
#8819=ORIENTED_EDGE ( 'NONE', *, *, #1563, .T. ) ;
#8829=VERTEX_POINT ( 'NONE', #13562 ) ;
#8835=CARTESIAN_POINT ( 'NONE',  ( -33.99999999999997158, 3.000000000000000000, -22.99999999999999645 ) ) ;
#8837=CARTESIAN_POINT ( 'NONE',  ( -26.00000000000002842, 3.000000000000000000, 34.00000000000000711 ) ) ;
#8868=DIRECTION ( 'NONE',  ( -0.000000000000000000, -1.000000000000000000, -0.000000000000000000 ) ) ;
#8889=ORIENTED_EDGE ( 'NONE', *, *, #910, .F. ) ;
#8922=DIRECTION ( 'NONE',  ( -0.000000000000000000, -0.000000000000000000, 1.000000000000000000 ) ) ;
#8927=CYLINDRICAL_SURFACE ( 'NONE', #9629, 2.500000000000002220 ) ;
#8928=AXIS2_PLACEMENT_3D ( 'NONE', #6192, #12884, #14205 ) ;
#8929=DIRECTION ( 'NONE',  ( -0.000000000000000000, 1.000000000000000000, -0.000000000000000000 ) ) ;
#8951=LINE ( 'NONE', #4325, #17604 ) ;
#8956=ORIENTED_EDGE ( 'NONE', *, *, #13237, .F. ) ;
#8960=ORIENTED_EDGE ( 'NONE', *, *, #8965, .T. ) ;
#8965=EDGE_CURVE ( 'NONE', #14793, #16062, #2727, .T. ) ;
#8978=CARTESIAN_POINT ( 'NONE',  ( 40.00000000000003553, 3.000000000000000000, 26.00000000000000355 ) ) ;
#8983=SURFACE_STYLE_USAGE ( .BOTH. , #12091 ) ;
#8993=LINE ( 'NONE', #18152, #7078 ) ;
#9001=EDGE_CURVE ( 'NONE', #16198, #11769, #19578, .T. ) ;
#9035=DIRECTION ( 'NONE',  ( -0.000000000000000000, 1.000000000000000000, -0.000000000000000000 ) ) ;
#9047=VECTOR ( 'NONE', #11777, 1000.000000000000000 ) ;
#9063=CARTESIAN_POINT ( 'NONE',  ( 4.163799117101000559E-15, 23.00000000000000000, 34.00000000000000000 ) ) ;
#9086=CARTESIAN_POINT ( 'NONE',  ( -39.99999999999997868, -20.00000000000000000, -19.99999999999999645 ) ) ;
#9096=ORIENTED_EDGE ( 'NONE', *, *, #7636, .F. ) ;
#9098=( NAMED_UNIT ( * ) PLANE_ANGLE_UNIT ( ) SI_UNIT ( $, .RADIAN. ) );
#9119=ORIENTED_EDGE ( 'NONE', *, *, #1808, .F. ) ;
#9130=EDGE_CURVE ( 'NONE', #18073, #5054, #6132, .T. ) ;
#9133=CYLINDRICAL_SURFACE ( 'NONE', #19345, 4.999999999999997335 ) ;
#9135=CARTESIAN_POINT ( 'NONE',  ( -39.99999999999997868, 3.000000000000000000, 26.00000000000000355 ) ) ;
#9141=LINE ( 'NONE', #5759, #17422 ) ;
#9152=LINE ( 'NONE', #13591, #3103 ) ;
#9160=CARTESIAN_POINT ( 'NONE',  ( 37.00000000000003553, -20.00000000000000000, 20.00000000000000000 ) ) ;
#9180=ORIENTED_EDGE ( 'NONE', *, *, #1221, .T. ) ;
#9196=CARTESIAN_POINT ( 'NONE',  ( -26.00000000000002842, 0.000000000000000000, -39.99999999999999289 ) ) ;
#9211=ADVANCED_FACE ( 'NONE', ( #3757 ), #14567, .F. ) ;
#9213=ORIENTED_EDGE ( 'NONE', *, *, #7765, .F. ) ;
#9229=DIRECTION ( 'NONE',  ( 0.000000000000000000, 0.000000000000000000, -1.000000000000000000 ) ) ;
#9244=DIRECTION ( 'NONE',  ( 0.000000000000000000, 0.000000000000000000, -1.000000000000000000 ) ) ;
#9259=DIRECTION ( 'NONE',  ( 0.000000000000000000, 0.000000000000000000, 1.000000000000000000 ) ) ;
#9270=ORIENTED_EDGE ( 'NONE', *, *, #1808, .T. ) ;
#9280=CARTESIAN_POINT ( 'NONE',  ( 34.00000000000002842, -20.00000000000000000, 23.00000000000000355 ) ) ;
#9285=FILL_AREA_STYLE_COLOUR ( '', #15284 ) ;
#9305=CARTESIAN_POINT ( 'NONE',  ( 25.99999999999996092, 3.000000000000000000, 31.00000000000004263 ) ) ;
#9323=ORIENTED_EDGE ( 'NONE', *, *, #14911, .T. ) ;
#9339=DIRECTION ( 'NONE',  ( 0.000000000000000000, 0.000000000000000000, -1.000000000000000000 ) ) ;
#9346=VERTEX_POINT ( 'NONE', #16916 ) ;
#9366=DIRECTION ( 'NONE',  ( 0.000000000000000000, 0.000000000000000000, -1.000000000000000000 ) ) ;
#9374=EDGE_CURVE ( 'NONE', #2287, #6649, #14024, .T. ) ;
#9376=ORIENTED_EDGE ( 'NONE', *, *, #4304, .T. ) ;
#9390=ADVANCED_FACE ( 'NONE', ( #20187 ), #10725, .F. ) ;
#9395=CARTESIAN_POINT ( 'NONE',  ( -34.99999999999998579, -20.00000000000000000, 23.50000000000000711 ) ) ;
#9411=AXIS2_PLACEMENT_3D ( 'NONE', #12263, #20079, #12378 ) ;
#9425=VERTEX_POINT ( 'NONE', #13003 ) ;
#9428=VERTEX_POINT ( 'NONE', #7934 ) ;
#9446=DIRECTION ( 'NONE',  ( -0.000000000000000000, -1.000000000000000000, 0.000000000000000000 ) ) ;
#9448=CARTESIAN_POINT ( 'NONE',  ( -21.00000000000002842, 3.000000000000000000, -34.99999999999999289 ) ) ;
#9462=DIRECTION ( 'NONE',  ( -0.000000000000000000, 1.000000000000000000, -0.000000000000000000 ) ) ;
#9468=EDGE_CURVE ( 'NONE', #18509, #2620, #94, .T. ) ;
#9479=CARTESIAN_POINT ( 'NONE',  ( 34.00000000000002842, 3.000000000000000000, 23.00000000000000355 ) ) ;
#9485=DIRECTION ( 'NONE',  ( -0.000000000000000000, 1.000000000000000000, -0.000000000000000000 ) ) ;
#9488=ORIENTED_EDGE ( 'NONE', *, *, #15445, .F. ) ;
#9517=ORIENTED_EDGE ( 'NONE', *, *, #17520, .T. ) ;
#9527=DIRECTION ( 'NONE',  ( -1.000000000000000000, 0.000000000000000000, 0.000000000000000000 ) ) ;
#9530=EDGE_CURVE ( 'NONE', #16461, #9609, #1153, .T. ) ;
#9601=EDGE_LOOP ( 'NONE', ( #19496, #14017, #8420, #2946 ) ) ;
#9609=VERTEX_POINT ( 'NONE', #5356 ) ;
#9626=DIRECTION ( 'NONE',  ( 1.000000000000000000, -0.000000000000000000, 0.000000000000000000 ) ) ;
#9629=AXIS2_PLACEMENT_3D ( 'NONE', #11833, #9035, #1067 ) ;
#9632=DIRECTION ( 'NONE',  ( -1.000000000000000000, -0.000000000000000000, -0.000000000000000000 ) ) ;
#9649=VECTOR ( 'NONE', #16312, 1000.000000000000000 ) ;
#9658=LINE ( 'NONE', #1706, #318 ) ;
#9659=CARTESIAN_POINT ( 'NONE',  ( 34.00000000000002842, -20.00000000000000000, 26.00000000000000355 ) ) ;
#9666=( NAMED_UNIT ( * ) SI_UNIT ( $, .STERADIAN. ) SOLID_ANGLE_UNIT ( ) );
#9684=DIRECTION ( 'NONE',  ( 0.000000000000000000, 0.000000000000000000, 1.000000000000000000 ) ) ;
#9699=AXIS2_PLACEMENT_3D ( 'NONE', #20324, #10855, #5914 ) ;
#9710=AXIS2_PLACEMENT_3D ( 'NONE', #7344, #5293, #10327 ) ;
#9716=CARTESIAN_POINT ( 'NONE',  ( 4.163799117101000559E-15, 0.000000000000000000, 34.00000000000000000 ) ) ;
#9724=CYLINDRICAL_SURFACE ( 'NONE', #13829, 3.000000000000002665 ) ;
#9757=VERTEX_POINT ( 'NONE', #367 ) ;
#9758=EDGE_CURVE ( 'NONE', #7437, #1029, #6683, .T. ) ;
#9767=DIRECTION ( 'NONE',  ( 0.000000000000000000, 0.000000000000000000, 1.000000000000000000 ) ) ;
#9785=EDGE_LOOP ( 'NONE', ( #7909, #16432, #18187, #2282 ) ) ;
#9793=DIRECTION ( 'NONE',  ( -0.000000000000000000, 1.000000000000000000, -0.000000000000000000 ) ) ;
#9835=ORIENTED_EDGE ( 'NONE', *, *, #10108, .F. ) ;
#9848=EDGE_CURVE ( 'NONE', #2620, #16062, #6165, .T. ) ;
#9854=CARTESIAN_POINT ( 'NONE',  ( 0.000000000000000000, 50.00000000000000000, -36.50000000000000000 ) ) ;
#9868=VERTEX_POINT ( 'NONE', #17789 ) ;
#9870=DIRECTION ( 'NONE',  ( 1.000000000000000000, 0.000000000000000000, -0.000000000000000000 ) ) ;
#9878=DIRECTION ( 'NONE',  ( 0.000000000000000000, 0.000000000000000000, -1.000000000000000000 ) ) ;
#9934=ORIENTED_EDGE ( 'NONE', *, *, #10295, .F. ) ;
#9936=EDGE_LOOP ( 'NONE', ( #17753, #7487, #2061, #4826 ) ) ;
#9970=CARTESIAN_POINT ( 'NONE',  ( -23.00000000000003197, 0.000000000000000000, 37.00000000000000711 ) ) ;
#9992=LINE ( 'NONE', #19644, #19540 ) ;
#9999=DIRECTION ( 'NONE',  ( 0.000000000000000000, 0.000000000000000000, -1.000000000000000000 ) ) ;
#10000=CARTESIAN_POINT ( 'NONE',  ( 22.99999999999995737, 3.000000000000000000, -33.99999999999998579 ) ) ;
#10021=ORIENTED_EDGE ( 'NONE', *, *, #13545, .T. ) ;
#10036=DIRECTION ( 'NONE',  ( 1.000000000000000000, 0.000000000000000000, 0.000000000000000000 ) ) ;
#10066=ORIENTED_EDGE ( 'NONE', *, *, #11697, .F. ) ;
#10078=CARTESIAN_POINT ( 'NONE',  ( 25.99999999999996092, 3.000000000000000000, 31.00000000000004263 ) ) ;
#10079=VECTOR ( 'NONE', #19156, 1000.000000000000000 ) ;
#10104=CARTESIAN_POINT ( 'NONE',  ( -20.00000000000003197, 3.000000000000000000, 37.00000000000000711 ) ) ;
#10106=CARTESIAN_POINT ( 'NONE',  ( -39.99999999999997868, 3.000000000000000000, 26.00000000000000355 ) ) ;
#10108=EDGE_CURVE ( 'NONE', #3089, #10871, #15835, .T. ) ;
#10132=CARTESIAN_POINT ( 'NONE',  ( -34.99999999999998579, 0.000000000000000000, 21.00000000000000355 ) ) ;
#10181=AXIS2_PLACEMENT_3D ( 'NONE', #8978, #1402, #12467 ) ;
#10210=CARTESIAN_POINT ( 'NONE',  ( 25.99999999999996092, 0.000000000000000000, 40.00000000000000711 ) ) ;
#10231=ORIENTED_EDGE ( 'NONE', *, *, #6471, .F. ) ;
#10238=CARTESIAN_POINT ( 'NONE',  ( -20.00000000000003197, 3.000000000000000000, 37.00000000000000711 ) ) ;
#10241=PLANE ( 'NONE',  #2130 ) ;
#10268=LINE ( 'NONE', #10078, #13247 ) ;
#10287=VERTEX_POINT ( 'NONE', #16838 ) ;
#10295=EDGE_CURVE ( 'NONE', #3014, #17794, #8993, .T. ) ;
#10317=LINE ( 'NONE', #16630, #20177 ) ;
#10323=CARTESIAN_POINT ( 'NONE',  ( -26.00000000000002842, 0.000000000000000000, 34.00000000000000711 ) ) ;
#10327=DIRECTION ( 'NONE',  ( -1.000000000000000000, 0.000000000000000000, -0.000000000000000000 ) ) ;
#10361=ORIENTED_EDGE ( 'NONE', *, *, #8155, .F. ) ;
#10370=CARTESIAN_POINT ( 'NONE',  ( -36.99999999999997868, 0.000000000000000000, -22.99999999999999645 ) ) ;
#10380=SHAPE_REPRESENTATION ( 'Servo-Bas', ( #2741 ), #14258 ) ;
#10399=EDGE_LOOP ( 'NONE', ( #13660, #8475, #7376, #6196 ) ) ;
#10439=LINE ( 'NONE', #7461, #2095 ) ;
#10444=DIRECTION ( 'NONE',  ( -0.000000000000000000, -1.000000000000000000, -0.000000000000000000 ) ) ;
#10473=CARTESIAN_POINT ( 'NONE',  ( -39.99999999999997868, 3.000000000000000000, -19.99999999999999645 ) ) ;
#10483=UNCERTAINTY_MEASURE_WITH_UNIT (LENGTH_MEASURE( 1.000000000000000082E-05 ), #15679, 'distance_accuracy_value', 'NONE');
#10494=LINE ( 'NONE', #9063, #7787 ) ;
#10499=ADVANCED_FACE ( 'NONE', ( #6843 ), #6631, .T. ) ;
#10515=VERTEX_POINT ( 'NONE', #424 ) ;
#10529=LINE ( 'NONE', #20092, #19858 ) ;
#10533=EDGE_LOOP ( 'NONE', ( #8246, #11388 ) ) ;
#10550=ADVANCED_FACE ( 'NONE', ( #4227 ), #19961, .F. ) ;
#10577=LINE ( 'NONE', #8835, #7185 ) ;
#10586=EDGE_LOOP ( 'NONE', ( #15996, #9213 ) ) ;
#10596=DIRECTION ( 'NONE',  ( 0.000000000000000000, 1.000000000000000000, 0.000000000000000000 ) ) ;
#10607=EDGE_CURVE ( 'NONE', #19010, #688, #16797, .T. ) ;
#10639=ORIENTED_EDGE ( 'NONE', *, *, #13428, .T. ) ;
#10646=EDGE_CURVE ( 'NONE', #12110, #9346, #19899, .T. ) ;
#10682=CIRCLE ( 'NONE', #6421, 34.00000000000000000 ) ;
#10684=FACE_OUTER_BOUND ( 'NONE', #18471, .T. ) ;
#10695=AXIS2_PLACEMENT_3D ( 'NONE', #12148, #10596, #15562 ) ;
#10725=PLANE ( 'NONE',  #9411 ) ;
#10735=CARTESIAN_POINT ( 'NONE',  ( -20.00000000000003197, 3.000000000000000000, 37.00000000000000711 ) ) ;
#10762=PRODUCT_CONTEXT ( 'NONE', #6316, 'mechanical' ) ;
#10771=VERTEX_POINT ( 'NONE', #6690 ) ;
#10777=CARTESIAN_POINT ( 'NONE',  ( 4.163799117101000559E-15, 16.00000000000000000, 34.00000000000000000 ) ) ;
#10779=EDGE_CURVE ( 'NONE', #7206, #5094, #490, .T. ) ;
#10784=DIRECTION ( 'NONE',  ( -0.000000000000000000, -1.000000000000000000, -0.000000000000000000 ) ) ;
#10793=VERTEX_POINT ( 'NONE', #8520 ) ;
#10806=DIRECTION ( 'NONE',  ( 0.000000000000000000, 0.000000000000000000, 1.000000000000000000 ) ) ;
#10808=AXIS2_PLACEMENT_3D ( 'NONE', #11494, #3571, #2408 ) ;
#10831=LINE ( 'NONE', #9395, #1436 ) ;
#10855=DIRECTION ( 'NONE',  ( -0.000000000000000000, -1.000000000000000000, -0.000000000000000000 ) ) ;
#10868=VERTEX_POINT ( 'NONE', #10473 ) ;
#10871=VERTEX_POINT ( 'NONE', #2737 ) ;
#10878=DIRECTION ( 'NONE',  ( -0.000000000000000000, -1.000000000000000000, -0.000000000000000000 ) ) ;
#10895=EDGE_CURVE ( 'NONE', #10771, #18631, #3937, .T. ) ;
#10905=ORIENTED_EDGE ( 'NONE', *, *, #5419, .T. ) ;
#10941=LINE ( 'NONE', #9280, #14303 ) ;
#10960=CARTESIAN_POINT ( 'NONE',  ( -31.00000000000006750, 0.000000000000000000, 26.00000000000000355 ) ) ;
#10964=VECTOR ( 'NONE', #6566, 1000.000000000000000 ) ;
#10993=PLANE ( 'NONE',  #16569 ) ;
#11009=ORIENTED_EDGE ( 'NONE', *, *, #10895, .F. ) ;
#11029=AXIS2_PLACEMENT_3D ( 'NONE', #683, #5448, #11737 ) ;
#11067=DIRECTION ( 'NONE',  ( 0.000000000000000000, 1.000000000000000000, 0.000000000000000000 ) ) ;
#11068=EDGE_LOOP ( 'NONE', ( #9270, #690, #19372, #5378 ) ) ;
#11070=FACE_OUTER_BOUND ( 'NONE', #4196, .T. ) ;
#11082=DIRECTION ( 'NONE',  ( -0.000000000000000000, -1.000000000000000000, 0.000000000000000000 ) ) ;
#11094=CARTESIAN_POINT ( 'NONE',  ( -31.00000000000003197, 3.000000000000000000, -30.99999999999999289 ) ) ;
#11112=FACE_BOUND ( 'NONE', #14327, .T. ) ;
#11115=DIRECTION ( 'NONE',  ( -0.000000000000000000, 1.000000000000000000, -0.000000000000000000 ) ) ;
#11118=PLANE ( 'NONE',  #8928 ) ;
#11127=VECTOR ( 'NONE', #16779, 1000.000000000000000 ) ;
#11130=DIRECTION ( 'NONE',  ( -0.000000000000000000, 1.000000000000000000, -0.000000000000000000 ) ) ;
#11138=ORIENTED_EDGE ( 'NONE', *, *, #13715, .T. ) ;
#11151=CARTESIAN_POINT ( 'NONE',  ( -31.00000000000006395, 0.000000000000000000, -25.99999999999999645 ) ) ;
#11167=ORIENTED_EDGE ( 'NONE', *, *, #6008, .F. ) ;
#11169=VECTOR ( 'NONE', #19438, 1000.000000000000000 ) ;
#11187=DIRECTION ( 'NONE',  ( 0.000000000000000000, 1.000000000000000000, 0.000000000000000000 ) ) ;
#11190=LINE ( 'NONE', #845, #8706 ) ;
#11192=CARTESIAN_POINT ( 'NONE',  ( -26.00000000000002842, 0.000000000000000000, 31.00000000000003908 ) ) ;
#11207=CARTESIAN_POINT ( 'NONE',  ( -21.00000000000002842, 3.000000000000000000, -34.99999999999999289 ) ) ;
#11214=VERTEX_POINT ( 'NONE', #9305 ) ;
#11243=DIRECTION ( 'NONE',  ( 0.000000000000000000, 0.000000000000000000, 1.000000000000000000 ) ) ;
#11259=ORIENTED_EDGE ( 'NONE', *, *, #3207, .T. ) ;
#11267=ORIENTED_EDGE ( 'NONE', *, *, #12799, .F. ) ;
#11271=AXIS2_PLACEMENT_3D ( 'NONE', #18348, #7243, #16158 ) ;
#11272=VERTEX_POINT ( 'NONE', #14055 ) ;
#11296=VECTOR ( 'NONE', #16637, 1000.000000000000000 ) ;
#11310=DIRECTION ( 'NONE',  ( 0.000000000000000000, -0.000000000000000000, -1.000000000000000000 ) ) ;
#11321=VERTEX_POINT ( 'NONE', #6226 ) ;
#11322=VECTOR ( 'NONE', #6245, 1000.000000000000000 ) ;
#11326=ORIENTED_EDGE ( 'NONE', *, *, #6975, .F. ) ;
#11347=LINE ( 'NONE', #17933, #3455 ) ;
#11354=VECTOR ( 'NONE', #5871, 1000.000000000000000 ) ;
#11375=CYLINDRICAL_SURFACE ( 'NONE', #20080, 2.500000000000002220 ) ;
#11377=CIRCLE ( 'NONE', #14009, 3.000000000000002665 ) ;
#11388=ORIENTED_EDGE ( 'NONE', *, *, #10646, .F. ) ;
#11400=FACE_OUTER_BOUND ( 'NONE', #6174, .T. ) ;
#11425=CARTESIAN_POINT ( 'NONE',  ( -33.99999999999997158, 3.000000000000000000, -22.99999999999999645 ) ) ;
#11432=ORIENTED_EDGE ( 'NONE', *, *, #5403, .F. ) ;
#11435=VERTEX_POINT ( 'NONE', #8283 ) ;
#11457=ADVANCED_FACE ( 'NONE', ( #5896 ), #16927, .F. ) ;
#11494=CARTESIAN_POINT ( 'NONE',  ( 22.99999999999995737, 0.000000000000000000, -36.99999999999999289 ) ) ;
#11502=VERTEX_POINT ( 'NONE', #920 ) ;
#11552=AXIS2_PLACEMENT_3D ( 'NONE', #2818, #7968, #130 ) ;
#11564=ORIENTED_EDGE ( 'NONE', *, *, #3187, .T. ) ;
#11587=LINE ( 'NONE', #10238, #16278 ) ;
#11592=VERTEX_POINT ( 'NONE', #17510 ) ;
#11633=ADVANCED_FACE ( 'NONE', ( #8 ), #6110, .F. ) ;
#11644=CARTESIAN_POINT ( 'NONE',  ( -39.99999999999997868, 3.000000000000000000, 26.00000000000000355 ) ) ;
#11645=VECTOR ( 'NONE', #18016, 1000.000000000000000 ) ;
#11671=CARTESIAN_POINT ( 'NONE',  ( 40.00000000000003553, 3.000000000000000000, -25.99999999999999645 ) ) ;
#11672=LINE ( 'NONE', #17951, #18844 ) ;
#11678=DIRECTION ( 'NONE',  ( -0.000000000000000000, 1.000000000000000000, -0.000000000000000000 ) ) ;
#11697=EDGE_CURVE ( 'NONE', #1451, #13169, #7943, .T. ) ;
#11707=CARTESIAN_POINT ( 'NONE',  ( -33.99999999999997158, -20.00000000000000000, -22.99999999999999645 ) ) ;
#11723=ORIENTED_EDGE ( 'NONE', *, *, #16119, .F. ) ;
#11730=PLANE ( 'NONE',  #1349 ) ;
#11737=DIRECTION ( 'NONE',  ( 0.000000000000000000, 0.000000000000000000, -1.000000000000000000 ) ) ;
#11739=DIRECTION ( 'NONE',  ( -0.000000000000000000, -1.000000000000000000, 0.000000000000000000 ) ) ;
#11750=AXIS2_PLACEMENT_3D ( 'NONE', #11921, #18185, #6983 ) ;
#11759=PLANE ( 'NONE',  #19328 ) ;
#11761=CARTESIAN_POINT ( 'NONE',  ( -26.00000000000002842, 3.000000000000000000, 34.00000000000000711 ) ) ;
#11769=VERTEX_POINT ( 'NONE', #5372 ) ;
#11771=EDGE_CURVE ( 'NONE', #18646, #12714, #16317, .T. ) ;
#11777=DIRECTION ( 'NONE',  ( -0.000000000000000000, -1.000000000000000000, -0.000000000000000000 ) ) ;
#11786=DIRECTION ( 'NONE',  ( -0.000000000000000000, 1.000000000000000000, -0.000000000000000000 ) ) ;
#11823=VERTEX_POINT ( 'NONE', #16716 ) ;
#11833=CARTESIAN_POINT ( 'NONE',  ( -34.99999999999998579, -20.00000000000000000, 21.00000000000000355 ) ) ;
#11915=AXIS2_PLACEMENT_3D ( 'NONE', #13876, #969, #18310 ) ;
#11921=CARTESIAN_POINT ( 'NONE',  ( 35.00000000000003553, 3.000000000000000000, -20.99999999999999645 ) ) ;
#11922=ORIENTED_EDGE ( 'NONE', *, *, #8773, .F. ) ;
#11924=CARTESIAN_POINT ( 'NONE',  ( -39.99999999999997868, 0.000000000000000000, 26.00000000000000355 ) ) ;
#11927=ADVANCED_FACE ( 'NONE', ( #11400 ), #7616, .F. ) ;
#11965=VERTEX_POINT ( 'NONE', #5015 ) ;
#11978=CARTESIAN_POINT ( 'NONE',  ( -31.00000000000006750, 3.000000000000000000, 26.00000000000000355 ) ) ;
#12091=SURFACE_SIDE_STYLE ('',( #5808 ) ) ;
#12110=VERTEX_POINT ( 'NONE', #5779 ) ;
#12117=ORIENTED_EDGE ( 'NONE', *, *, #13428, .F. ) ;
#12132=LINE ( 'NONE', #16991, #2276 ) ;
#12148=CARTESIAN_POINT ( 'NONE',  ( 0.000000000000000000, 3.000000000000000000, 0.000000000000000000 ) ) ;
#12194=CARTESIAN_POINT ( 'NONE',  ( 30.99999999999999645, 3.000000000000000000, 26.00000000000000355 ) ) ;
#12229=ORIENTED_EDGE ( 'NONE', *, *, #16119, .T. ) ;
#12256=AXIS2_PLACEMENT_3D ( 'NONE', #6156, #9626, #12631 ) ;
#12257=ORIENTED_EDGE ( 'NONE', *, *, #3120, .F. ) ;
#12263=CARTESIAN_POINT ( 'NONE',  ( 34.00000000000002842, -20.00000000000000000, 23.00000000000000355 ) ) ;
#12285=DIRECTION ( 'NONE',  ( 0.000000000000000000, 0.000000000000000000, -1.000000000000000000 ) ) ;
#12296=CARTESIAN_POINT ( 'NONE',  ( 4.469960816887838430E-15, 26.00000000000000000, 36.50000000000000000 ) ) ;
#12313=AXIS2_PLACEMENT_3D ( 'NONE', #10735, #18253, #2493 ) ;
#12338=DIRECTION ( 'NONE',  ( -0.000000000000000000, -1.000000000000000000, 0.000000000000000000 ) ) ;
#12357=ORIENTED_EDGE ( 'NONE', *, *, #16373, .T. ) ;
#12367=FACE_OUTER_BOUND ( 'NONE', #13158, .T. ) ;
#12377=ORIENTED_EDGE ( 'NONE', *, *, #19336, .T. ) ;
#12378=DIRECTION ( 'NONE',  ( 0.000000000000000000, 0.000000000000000000, 1.000000000000000000 ) ) ;
#12467=DIRECTION ( 'NONE',  ( 0.000000000000000000, 0.000000000000000000, 1.000000000000000000 ) ) ;
#12497=ORIENTED_EDGE ( 'NONE', *, *, #4090, .F. ) ;
#12520=ORIENTED_EDGE ( 'NONE', *, *, #13975, .F. ) ;
#12524=ORIENTED_EDGE ( 'NONE', *, *, #5140, .F. ) ;
#12537=CARTESIAN_POINT ( 'NONE',  ( -21.00000000000002842, 0.000000000000000000, -34.99999999999999289 ) ) ;
#12543=ORIENTED_EDGE ( 'NONE', *, *, #9530, .T. ) ;
#12560=DIRECTION ( 'NONE',  ( 0.000000000000000000, 0.000000000000000000, 1.000000000000000000 ) ) ;
#12572=ORIENTED_EDGE ( 'NONE', *, *, #10108, .T. ) ;
#12585=DIRECTION ( 'NONE',  ( 0.000000000000000000, 0.000000000000000000, -1.000000000000000000 ) ) ;
#12606=DIRECTION ( 'NONE',  ( 1.000000000000000000, 0.000000000000000000, 0.000000000000000000 ) ) ;
#12607=ORIENTED_EDGE ( 'NONE', *, *, #9468, .T. ) ;
#12617=EDGE_CURVE ( 'NONE', #9609, #16461, #5089, .T. ) ;
#12623=ORIENTED_EDGE ( 'NONE', *, *, #13345, .T. ) ;
#12631=DIRECTION ( 'NONE',  ( 0.000000000000000000, 0.000000000000000000, -1.000000000000000000 ) ) ;
#12665=ORIENTED_EDGE ( 'NONE', *, *, #13196, .T. ) ;
#12714=VERTEX_POINT ( 'NONE', #8592 ) ;
#12722=AXIS2_PLACEMENT_3D ( 'NONE', #3405, #17625, #9684 ) ;
#12735=ORIENTED_EDGE ( 'NONE', *, *, #16373, .F. ) ;
#12748=CARTESIAN_POINT ( 'NONE',  ( -26.00000000000002842, 3.000000000000000000, -39.99999999999999289 ) ) ;
#12752=FACE_OUTER_BOUND ( 'NONE', #8170, .T. ) ;
#12792=ADVANCED_FACE ( 'NONE', ( #29 ), #18584, .F. ) ;
#12799=EDGE_CURVE ( 'NONE', #3014, #5094, #6021, .T. ) ;
#12800=DIRECTION ( 'NONE',  ( -0.000000000000000000, 1.000000000000000000, -0.000000000000000000 ) ) ;
#12807=DIRECTION ( 'NONE',  ( 0.000000000000000000, 0.000000000000000000, 1.000000000000000000 ) ) ;
#12814=EDGE_CURVE ( 'NONE', #9609, #12110, #14057, .T. ) ;
#12884=DIRECTION ( 'NONE',  ( 0.000000000000000000, 1.000000000000000000, 0.000000000000000000 ) ) ;
#12885=CARTESIAN_POINT ( 'NONE',  ( 20.99999999999996092, 3.000000000000000000, 35.00000000000000711 ) ) ;
#12894=VERTEX_POINT ( 'NONE', #20117 ) ;
#12905=FACE_OUTER_BOUND ( 'NONE', #10399, .T. ) ;
#12918=CARTESIAN_POINT ( 'NONE',  ( 0.000000000000000000, 26.00000000000000000, 0.000000000000000000 ) ) ;
#12937=VERTEX_POINT ( 'NONE', #19192 ) ;
#12943=VERTEX_POINT ( 'NONE', #5093 ) ;
#12974=CARTESIAN_POINT ( 'NONE',  ( 19.99999999999995381, 0.000000000000000000, -36.99999999999999289 ) ) ;
#12984=DIRECTION ( 'NONE',  ( -0.000000000000000000, 1.000000000000000000, -0.000000000000000000 ) ) ;
#12993=CYLINDRICAL_SURFACE ( 'NONE', #2996, 34.00000000000000000 ) ;
#12995=VECTOR ( 'NONE', #17531, 1000.000000000000000 ) ;
#12996=EDGE_CURVE ( 'NONE', #5054, #18073, #3454, .T. ) ;
#13003=CARTESIAN_POINT ( 'NONE',  ( 25.99999999999996092, 3.000000000000000000, 40.00000000000000711 ) ) ;
#13018=VECTOR ( 'NONE', #12606, 1000.000000000000000 ) ;
#13047=EDGE_LOOP ( 'NONE', ( #5886, #3195 ) ) ;
#13051=VECTOR ( 'NONE', #19926, 1000.000000000000000 ) ;
#13070=CARTESIAN_POINT ( 'NONE',  ( 25.99999999999996092, 3.000000000000000000, -33.99999999999998579 ) ) ;
#13078=ADVANCED_FACE ( 'NONE', ( #634 ), #13344, .F. ) ;
#13099=DIRECTION ( 'NONE',  ( 0.000000000000000000, 0.000000000000000000, -1.000000000000000000 ) ) ;
#13106=VECTOR ( 'NONE', #307, 1000.000000000000000 ) ;
#13116=DIRECTION ( 'NONE',  ( -0.000000000000000000, -1.000000000000000000, 0.000000000000000000 ) ) ;
#13135=DIRECTION ( 'NONE',  ( 0.000000000000000000, 0.000000000000000000, -1.000000000000000000 ) ) ;
#13138=DIRECTION ( 'NONE',  ( 0.000000000000000000, 0.000000000000000000, 1.000000000000000000 ) ) ;
#13148=AXIS2_PLACEMENT_3D ( 'NONE', #16531, #11786, #17754 ) ;
#13158=EDGE_LOOP ( 'NONE', ( #13781, #4052, #16073, #824 ) ) ;
#13168=AXIS2_PLACEMENT_3D ( 'NONE', #1360, #18705, #2840 ) ;
#13169=VERTEX_POINT ( 'NONE', #15876 ) ;
#13196=EDGE_CURVE ( 'NONE', #15883, #10771, #19894, .T. ) ;
#13209=LINE ( 'NONE', #10104, #9649 ) ;
#13222=ORIENTED_EDGE ( 'NONE', *, *, #10607, .T. ) ;
#13228=DIRECTION ( 'NONE',  ( 0.000000000000000000, 0.000000000000000000, -1.000000000000000000 ) ) ;
#13237=EDGE_CURVE ( 'NONE', #5387, #5210, #1124, .T. ) ;
#13247=VECTOR ( 'NONE', #5240, 1000.000000000000000 ) ;
#13254=CARTESIAN_POINT ( 'NONE',  ( 30.99999999999999645, 3.000000000000000000, -25.99999999999999645 ) ) ;
#13273=CARTESIAN_POINT ( 'NONE',  ( 37.00000000000003553, 3.000000000000000000, 23.00000000000000355 ) ) ;
#13284=EDGE_CURVE ( 'NONE', #6649, #3049, #4935, .T. ) ;
#13286=CARTESIAN_POINT ( 'NONE',  ( -36.99999999999997868, 3.000000000000000000, -19.99999999999999289 ) ) ;
#13287=CARTESIAN_POINT ( 'NONE',  ( -31.00000000000003197, 0.000000000000000000, -30.99999999999999289 ) ) ;
#13300=ORIENTED_EDGE ( 'NONE', *, *, #14158, .F. ) ;
#13327=EDGE_LOOP ( 'NONE', ( #9517, #12257, #11167, #11138 ) ) ;
#13344=PLANE ( 'NONE',  #9710 ) ;
#13345=EDGE_CURVE ( 'NONE', #6404, #10287, #8235, .T. ) ;
#13368=FACE_OUTER_BOUND ( 'NONE', #11068, .T. ) ;
#13390=DIRECTION ( 'NONE',  ( 0.000000000000000000, 0.000000000000000000, 1.000000000000000000 ) ) ;
#13410=PLANE ( 'NONE',  #18098 ) ;
#13413=LINE ( 'NONE', #11644, #15021 ) ;
#13428=EDGE_CURVE ( 'NONE', #9757, #18631, #14722, .T. ) ;
#13431=EDGE_CURVE ( 'NONE', #15689, #3089, #13585, .T. ) ;
#13441=EDGE_CURVE ( 'NONE', #12894, #14969, #8338, .T. ) ;
#13471=VERTEX_POINT ( 'NONE', #13286 ) ;
#13476=ORIENTED_EDGE ( 'NONE', *, *, #8240, .T. ) ;
#13483=CARTESIAN_POINT ( 'NONE',  ( -26.00000000000002842, 0.000000000000000000, -31.00000000000003197 ) ) ;
#13487=CARTESIAN_POINT ( 'NONE',  ( -39.99999999999997868, 3.000000000000000000, -19.99999999999999645 ) ) ;
#13490=EDGE_LOOP ( 'NONE', ( #6272, #12497 ) ) ;
#13525=CARTESIAN_POINT ( 'NONE',  ( 19.99999999999995381, 3.000000000000000000, -39.99999999999999289 ) ) ;
#13534=VERTEX_POINT ( 'NONE', #4606 ) ;
#13545=EDGE_CURVE ( 'NONE', #9428, #6211, #6026, .T. ) ;
#13562=CARTESIAN_POINT ( 'NONE',  ( -39.99999999999997868, 0.000000000000000000, -19.99999999999999645 ) ) ;
#13575=DIRECTION ( 'NONE',  ( 1.000000000000000000, -0.000000000000000000, 0.000000000000000000 ) ) ;
#13580=EDGE_CURVE ( 'NONE', #13534, #14656, #8654, .T. ) ;
#13585=CIRCLE ( 'NONE', #1355, 3.000000000000002665 ) ;
#13591=CARTESIAN_POINT ( 'NONE',  ( 19.99999999999995381, 3.000000000000000000, -36.99999999999999289 ) ) ;
#13603=ADVANCED_FACE ( 'NONE', ( #8001, #6264, #15656, #1367, #13989, #20351 ), #10993, .F. ) ;
#13625=LINE ( 'NONE', #18259, #17083 ) ;
#13630=STYLED_ITEM ( 'NONE', ( #18354 ), #15739 ) ;
#13643=EDGE_LOOP ( 'NONE', ( #11564, #13300, #11326, #15319 ) ) ;
#13660=ORIENTED_EDGE ( 'NONE', *, *, #15566, .T. ) ;
#13715=EDGE_CURVE ( 'NONE', #9425, #7477, #5020, .T. ) ;
#13727=DIRECTION ( 'NONE',  ( -1.156482317317870344E-15, 0.000000000000000000, 1.000000000000000000 ) ) ;
#13743=CARTESIAN_POINT ( 'NONE',  ( -21.00000000000002842, 0.000000000000000000, -32.49999999999999289 ) ) ;
#13746=AXIS2_PLACEMENT_3D ( 'NONE', #16389, #3989, #13099 ) ;
#13754=ORIENTED_EDGE ( 'NONE', *, *, #1268, .F. ) ;
#13781=ORIENTED_EDGE ( 'NONE', *, *, #18220, .F. ) ;
#13800=CIRCLE ( 'NONE', #15134, 4.999999999999997335 ) ;
#13808=DIRECTION ( 'NONE',  ( -1.000000000000000000, -0.000000000000000000, -0.000000000000000000 ) ) ;
#13828=EDGE_CURVE ( 'NONE', #14969, #1468, #81, .T. ) ;
#13829=AXIS2_PLACEMENT_3D ( 'NONE', #17538, #3916, #3439 ) ;
#13851=EDGE_CURVE ( 'NONE', #18631, #19010, #11672, .T. ) ;
#13876=CARTESIAN_POINT ( 'NONE',  ( 30.99999999999996092, 3.000000000000000000, -30.99999999999999289 ) ) ;
#13885=ORIENTED_EDGE ( 'NONE', *, *, #16689, .T. ) ;
#13894=CARTESIAN_POINT ( 'NONE',  ( -31.00000000000002842, 3.000000000000000000, 31.00000000000000000 ) ) ;
#13926=CLOSED_SHELL ( 'NONE', ( #4112, #2935, #5648, #17065, #10499, #17386, #6396, #3099, #4459, #8357, #3938, #20046, #14420, #11457, #8250, #11633, #7148, #6172, #3791, #12792, #18554, #10550, #9211, #14974, #3704, #6089, #15348, #13078, #16105, #13603, #4120, #14128, #8637, #18054, #5088, #16676, #6365, #3511, #14495, #4589, #11927, #9390, #17224, #16932 ) ) ;
#13975=EDGE_CURVE ( 'NONE', #17548, #13169, #4039, .T. ) ;
#13976=AXIS2_PLACEMENT_3D ( 'NONE', #13273, #19520, #5441 ) ;
#13989=FACE_BOUND ( 'NONE', #10533, .T. ) ;
#13996=EDGE_LOOP ( 'NONE', ( #2339, #2651, #743, #9180 ) ) ;
#14001=AXIS2_PLACEMENT_3D ( 'NONE', #18907, #9527, #1889 ) ;
#14009=AXIS2_PLACEMENT_3D ( 'NONE', #10370, #3887, #12285 ) ;
#14017=ORIENTED_EDGE ( 'NONE', *, *, #9001, .T. ) ;
#14024=LINE ( 'NONE', #20292, #2811 ) ;
#14025=AXIS2_PLACEMENT_3D ( 'NONE', #16355, #2085, #552 ) ;
#14043=CARTESIAN_POINT ( 'NONE',  ( 0.000000000000000000, 16.00000000000000000, 0.000000000000000000 ) ) ;
#14055=CARTESIAN_POINT ( 'NONE',  ( -26.00000000000002842, 0.000000000000000000, -39.99999999999999289 ) ) ;
#14057=LINE ( 'NONE', #12296, #18251 ) ;
#14089=ORIENTED_EDGE ( 'NONE', *, *, #19336, .F. ) ;
#14095=ORIENTED_EDGE ( 'NONE', *, *, #13441, .F. ) ;
#14099=CIRCLE ( 'NONE', #10808, 3.000000000000002665 ) ;
#14128=ADVANCED_FACE ( 'NONE', ( #16208 ), #607, .T. ) ;
#14155=EDGE_CURVE ( 'NONE', #3606, #7437, #3824, .T. ) ;
#14158=EDGE_CURVE ( 'NONE', #14439, #18534, #13209, .T. ) ;
#14203=DIRECTION ( 'NONE',  ( 0.000000000000000000, 0.000000000000000000, 1.000000000000000000 ) ) ;
#14205=DIRECTION ( 'NONE',  ( 0.000000000000000000, -0.000000000000000000, 1.000000000000000000 ) ) ;
#14236=AXIS2_PLACEMENT_3D ( 'NONE', #18913, #11187, #15850 ) ;
#14241=CARTESIAN_POINT ( 'NONE',  ( 25.99999999999996092, 3.000000000000000000, 40.00000000000000711 ) ) ;
#14254=ORIENTED_EDGE ( 'NONE', *, *, #15018, .T. ) ;
#14258=( GEOMETRIC_REPRESENTATION_CONTEXT ( 3 ) GLOBAL_UNCERTAINTY_ASSIGNED_CONTEXT ( ( #10483 ) ) GLOBAL_UNIT_ASSIGNED_CONTEXT ( ( #15679, #1913, #9666 ) ) REPRESENTATION_CONTEXT ( 'NONE', 'WORKASPACE' ) );
#14276=CARTESIAN_POINT ( 'NONE',  ( 37.00000000000003553, -20.00000000000000000, 23.00000000000000355 ) ) ;
#14285=ADVANCED_BREP_SHAPE_REPRESENTATION ( '', ( #15739, #2741 ), #14258 ) ;
#14303=VECTOR ( 'NONE', #9485, 1000.000000000000000 ) ;
#14327=EDGE_LOOP ( 'NONE', ( #4479, #14592 ) ) ;
#14333=DIRECTION ( 'NONE',  ( 0.000000000000000000, 0.000000000000000000, -1.000000000000000000 ) ) ;
#14336=CARTESIAN_POINT ( 'NONE',  ( 19.99999999999995381, 3.000000000000000000, -36.99999999999999289 ) ) ;
#14337=FACE_OUTER_BOUND ( 'NONE', #13996, .T. ) ;
#14345=AXIS2_PLACEMENT_3D ( 'NONE', #16946, #20111, #6011 ) ;
#14359=CARTESIAN_POINT ( 'NONE',  ( 25.99999999999996092, 3.000000000000000000, -31.00000000000003197 ) ) ;
#14382=DIRECTION ( 'NONE',  ( 0.000000000000000000, 1.000000000000000000, 0.000000000000000000 ) ) ;
#14384=DIRECTION ( 'NONE',  ( 0.000000000000000000, 0.000000000000000000, 1.000000000000000000 ) ) ;
#14399=DIRECTION ( 'NONE',  ( -0.000000000000000000, -1.000000000000000000, -0.000000000000000000 ) ) ;
#14415=PLANE ( 'NONE',  #10181 ) ;
#14417=ORIENTED_EDGE ( 'NONE', *, *, #1503, .T. ) ;
#14420=ADVANCED_FACE ( 'NONE', ( #1479 ), #17368, .F. ) ;
#14433=EDGE_CURVE ( 'NONE', #3463, #10515, #3354, .T. ) ;
#14439=VERTEX_POINT ( 'NONE', #5125 ) ;
#14469=ORIENTED_EDGE ( 'NONE', *, *, #13431, .F. ) ;
#14493=EDGE_LOOP ( 'NONE', ( #199, #2612, #4281, #15279 ) ) ;
#14495=ADVANCED_FACE ( 'NONE', ( #13368 ), #10241, .F. ) ;
#14518=ORIENTED_EDGE ( 'NONE', *, *, #7653, .T. ) ;
#14520=AXIS2_PLACEMENT_3D ( 'NONE', #9160, #6672, #1895 ) ;
#14547=PLANE ( 'NONE',  #1923 ) ;
#14557=FACE_OUTER_BOUND ( 'NONE', #20050, .T. ) ;
#14567=CYLINDRICAL_SURFACE ( 'NONE', #19593, 2.999999999999995559 ) ;
#14592=ORIENTED_EDGE ( 'NONE', *, *, #13580, .F. ) ;
#14594=AXIS2_PLACEMENT_3D ( 'NONE', #2911, #1338, #15517 ) ;
#14629=ORIENTED_EDGE ( 'NONE', *, *, #18645, .F. ) ;
#14630=ORIENTED_EDGE ( 'NONE', *, *, #4078, .T. ) ;
#14643=DIRECTION ( 'NONE',  ( -0.000000000000000000, -1.000000000000000000, -0.000000000000000000 ) ) ;
#14656=VERTEX_POINT ( 'NONE', #13743 ) ;
#14659=FACE_OUTER_BOUND ( 'NONE', #13327, .T. ) ;
#14680=ORIENTED_EDGE ( 'NONE', *, *, #757, .T. ) ;
#14713=EDGE_CURVE ( 'NONE', #1029, #11272, #7663, .T. ) ;
#14722=LINE ( 'NONE', #284, #16871 ) ;
#14793=VERTEX_POINT ( 'NONE', #6753 ) ;
#14811=FACE_OUTER_BOUND ( 'NONE', #5647, .T. ) ;
#14822=EDGE_CURVE ( 'NONE', #12943, #11592, #19477, .T. ) ;
#14832=CIRCLE ( 'NONE', #1983, 2.500000000000002220 ) ;
#14837=DIRECTION ( 'NONE',  ( 0.000000000000000000, 0.000000000000000000, 1.000000000000000000 ) ) ;
#14881=VECTOR ( 'NONE', #8922, 1000.000000000000000 ) ;
#14897=EDGE_CURVE ( 'NONE', #11272, #4354, #10529, .T. ) ;
#14911=EDGE_CURVE ( 'NONE', #7206, #15689, #4345, .T. ) ;
#14936=ORIENTED_EDGE ( 'NONE', *, *, #13441, .T. ) ;
#14969=VERTEX_POINT ( 'NONE', #7543 ) ;
#14974=ADVANCED_FACE ( 'NONE', ( #19989 ), #5895, .F. ) ;
#14975=AXIS2_PLACEMENT_3D ( 'NONE', #127, #11067, #13138 ) ;
#14997=DIRECTION ( 'NONE',  ( -0.000000000000000000, 1.000000000000000000, -0.000000000000000000 ) ) ;
#15007=ORIENTED_EDGE ( 'NONE', *, *, #13851, .F. ) ;
#15018=EDGE_CURVE ( 'NONE', #1451, #5387, #15703, .T. ) ;
#15021=VECTOR ( 'NONE', #18111, 1000.000000000000000 ) ;
#15034=EDGE_CURVE ( 'NONE', #15689, #16657, #10941, .T. ) ;
#15039=ORIENTED_EDGE ( 'NONE', *, *, #13851, .T. ) ;
#15048=EDGE_CURVE ( 'NONE', #10793, #5054, #10831, .T. ) ;
#15114=LINE ( 'NONE', #11924, #18496 ) ;
#15134=AXIS2_PLACEMENT_3D ( 'NONE', #4300, #2848, #7500 ) ;
#15154=EDGE_LOOP ( 'NONE', ( #868, #12607, #2190, #2311 ) ) ;
#15157=AXIS2_PLACEMENT_3D ( 'NONE', #13894, #79, #9366 ) ;
#15174=FILL_AREA_STYLE ('',( #9285 ) ) ;
#15178=CIRCLE ( 'NONE', #3311, 36.50000000000000000 ) ;
#15193=ORIENTED_EDGE ( 'NONE', *, *, #10779, .F. ) ;
#15209=ORIENTED_EDGE ( 'NONE', *, *, #4740, .T. ) ;
#15222=CARTESIAN_POINT ( 'NONE',  ( -34.99999999999998579, 3.000000000000000000, 18.50000000000000355 ) ) ;
#15223=CARTESIAN_POINT ( 'NONE',  ( -20.00000000000003197, 0.000000000000000000, 37.00000000000000711 ) ) ;
#15259=CARTESIAN_POINT ( 'NONE',  ( 31.00000000000001776, 0.000000000000000000, -19.99999999999991473 ) ) ;
#15276=DIRECTION ( 'NONE',  ( 0.000000000000000000, 0.000000000000000000, 1.000000000000000000 ) ) ;
#15279=ORIENTED_EDGE ( 'NONE', *, *, #6624, .F. ) ;
#15280=( LENGTH_UNIT ( ) NAMED_UNIT ( * ) SI_UNIT ( .MILLI., .METRE. ) );
#15284=COLOUR_RGB ( '', 0.66274510, 0.83137255, 0.94901961) ;
#15316=VERTEX_POINT ( 'NONE', #16390 ) ;
#15319=ORIENTED_EDGE ( 'NONE', *, *, #13237, .T. ) ;
#15334=CARTESIAN_POINT ( 'NONE',  ( 30.99999999999996092, 3.000000000000000000, -30.99999999999999289 ) ) ;
#15348=ADVANCED_FACE ( 'NONE', ( #14811 ), #16289, .F. ) ;
#15375=DIRECTION ( 'NONE',  ( -0.000000000000000000, 1.000000000000000000, -0.000000000000000000 ) ) ;
#15381=CARTESIAN_POINT ( 'NONE',  ( 19.99999999999995381, 3.000000000000000000, -36.99999999999999289 ) ) ;
#15413=CARTESIAN_POINT ( 'NONE',  ( 30.99999999999999645, 0.000000000000000000, 26.00000000000000355 ) ) ;
#15445=EDGE_CURVE ( 'NONE', #19684, #17548, #7100, .T. ) ;
#15492=DIRECTION ( 'NONE',  ( -0.000000000000000000, -1.000000000000000000, 0.000000000000000000 ) ) ;
#15517=DIRECTION ( 'NONE',  ( 0.000000000000000000, 0.000000000000000000, 1.000000000000000000 ) ) ;
#15539=DIRECTION ( 'NONE',  ( 1.000000000000000000, 0.000000000000000000, 1.156482317317870344E-15 ) ) ;
#15562=DIRECTION ( 'NONE',  ( 0.000000000000000000, 0.000000000000000000, 1.000000000000000000 ) ) ;
#15566=EDGE_CURVE ( 'NONE', #12714, #19684, #11190, .T. ) ;
#15575=ORIENTED_EDGE ( 'NONE', *, *, #14897, .F. ) ;
#15583=EDGE_LOOP ( 'NONE', ( #12543, #2313 ) ) ;
#15588=VECTOR ( 'NONE', #1364, 1000.000000000000000 ) ;
#15589=LINE ( 'NONE', #17503, #10079 ) ;
#15620=CIRCLE ( 'NONE', #8689, 2.500000000000002220 ) ;
#15641=VECTOR ( 'NONE', #12807, 1000.000000000000000 ) ;
#15648=EDGE_CURVE ( 'NONE', #10793, #18104, #15620, .T. ) ;
#15656=FACE_BOUND ( 'NONE', #3402, .T. ) ;
#15678=AXIS2_PLACEMENT_3D ( 'NONE', #5000, #3150, #8095 ) ;
#15679=( LENGTH_UNIT ( ) NAMED_UNIT ( * ) SI_UNIT ( .MILLI., .METRE. ) );
#15688=EDGE_LOOP ( 'NONE', ( #16549, #3782, #10905, #357 ) ) ;
#15689=VERTEX_POINT ( 'NONE', #8483 ) ;
#15699=EDGE_CURVE ( 'NONE', #18646, #7052, #10439, .T. ) ;
#15703=LINE ( 'NONE', #1739, #7066 ) ;
#15715=ORIENTED_EDGE ( 'NONE', *, *, #18151, .F. ) ;
#15739=MANIFOLD_SOLID_BREP ( 'Boss-Extrude3', #13926 ) ;
#15743=CARTESIAN_POINT ( 'NONE',  ( 19.99999999999995381, 0.000000000000000000, -39.99999999999999289 ) ) ;
#15745=CIRCLE ( 'NONE', #1209, 2.500000000000002220 ) ;
#15754=CARTESIAN_POINT ( 'NONE',  ( -31.00000000000002842, 0.000000000000000000, 31.00000000000000000 ) ) ;
#15755=CARTESIAN_POINT ( 'NONE',  ( 30.99999999999995737, 3.000000000000000000, 31.00000000000000000 ) ) ;
#15756=DIRECTION ( 'NONE',  ( 0.000000000000000000, 1.000000000000000000, 0.000000000000000000 ) ) ;
#15763=ORIENTED_EDGE ( 'NONE', *, *, #15048, .T. ) ;
#15772=LINE ( 'NONE', #6693, #3565 ) ;
#15776=FACE_OUTER_BOUND ( 'NONE', #16008, .T. ) ;
#15789=PRODUCT_DEFINITION ( 'UNKNOWN', '', #17516, #5550 ) ;
#15805=DIRECTION ( 'NONE',  ( 0.000000000000000000, 0.000000000000000000, -1.000000000000000000 ) ) ;
#15823=AXIS2_PLACEMENT_3D ( 'NONE', #1354, #10878, #7884 ) ;
#15831=ORIENTED_EDGE ( 'NONE', *, *, #2189, .F. ) ;
#15835=LINE ( 'NONE', #3029, #11322 ) ;
#15850=DIRECTION ( 'NONE',  ( 0.000000000000000000, 0.000000000000000000, 1.000000000000000000 ) ) ;
#15868=CARTESIAN_POINT ( 'NONE',  ( -33.99999999999997158, 3.000000000000000000, -25.99999999999999645 ) ) ;
#15876=CARTESIAN_POINT ( 'NONE',  ( -26.00000000000002842, 0.000000000000000000, 34.00000000000000711 ) ) ;
#15877=FACE_OUTER_BOUND ( 'NONE', #15583, .T. ) ;
#15883=VERTEX_POINT ( 'NONE', #7845 ) ;
#15890=FACE_OUTER_BOUND ( 'NONE', #17445, .T. ) ;
#15936=ORIENTED_EDGE ( 'NONE', *, *, #6008, .T. ) ;
#15996=ORIENTED_EDGE ( 'NONE', *, *, #13828, .F. ) ;
#16008=EDGE_LOOP ( 'NONE', ( #19028, #3394, #6337, #20268 ) ) ;
#16062=VERTEX_POINT ( 'NONE', #18333 ) ;
#16071=EDGE_CURVE ( 'NONE', #11592, #10771, #8951, .T. ) ;
#16073=ORIENTED_EDGE ( 'NONE', *, *, #4510, .T. ) ;
#16105=ADVANCED_FACE ( 'NONE', ( #15776 ), #14415, .F. ) ;
#16111=DIRECTION ( 'NONE',  ( 0.000000000000000000, 0.000000000000000000, -1.000000000000000000 ) ) ;
#16116=DIRECTION ( 'NONE',  ( -0.000000000000000000, 1.000000000000000000, -0.000000000000000000 ) ) ;
#16119=EDGE_CURVE ( 'NONE', #11823, #11321, #8220, .T. ) ;
#16155=CARTESIAN_POINT ( 'NONE',  ( -20.00000000000003197, 3.000000000000000000, 40.00000000000000711 ) ) ;
#16158=DIRECTION ( 'NONE',  ( 0.000000000000000000, 0.000000000000000000, -1.000000000000000000 ) ) ;
#16159=DIRECTION ( 'NONE',  ( 0.000000000000000000, 0.000000000000000000, -1.000000000000000000 ) ) ;
#16189=DIRECTION ( 'NONE',  ( 0.000000000000000000, 0.000000000000000000, -1.000000000000000000 ) ) ;
#16198=VERTEX_POINT ( 'NONE', #8629 ) ;
#16208=FACE_OUTER_BOUND ( 'NONE', #7343, .T. ) ;
#16266=ORIENTED_EDGE ( 'NONE', *, *, #2560, .T. ) ;
#16273=ORIENTED_EDGE ( 'NONE', *, *, #16339, .T. ) ;
#16278=VECTOR ( 'NONE', #4062, 1000.000000000000000 ) ;
#16289=CYLINDRICAL_SURFACE ( 'NONE', #11029, 4.999999999999997335 ) ;
#16290=VECTOR ( 'NONE', #1230, 1000.000000000000000 ) ;
#16291=DIRECTION ( 'NONE',  ( -0.000000000000000000, -1.000000000000000000, -0.000000000000000000 ) ) ;
#16302=ORIENTED_EDGE ( 'NONE', *, *, #1528, .T. ) ;
#16312=DIRECTION ( 'NONE',  ( -0.000000000000000000, -1.000000000000000000, -0.000000000000000000 ) ) ;
#16317=LINE ( 'NONE', #10106, #2652 ) ;
#16339=EDGE_CURVE ( 'NONE', #11965, #10871, #9141, .T. ) ;
#16347=DIRECTION ( 'NONE',  ( -0.000000000000000000, -1.000000000000000000, 0.000000000000000000 ) ) ;
#16355=CARTESIAN_POINT ( 'NONE',  ( -34.99999999999998579, 3.000000000000000000, 21.00000000000000355 ) ) ;
#16367=DIRECTION ( 'NONE',  ( 0.000000000000000000, 0.000000000000000000, -1.000000000000000000 ) ) ;
#16373=EDGE_CURVE ( 'NONE', #6211, #3049, #12132, .T. ) ;
#16378=EDGE_CURVE ( 'NONE', #2143, #9868, #4276, .T. ) ;
#16380=ORIENTED_EDGE ( 'NONE', *, *, #10779, .T. ) ;
#16386=DIRECTION ( 'NONE',  ( -0.000000000000000000, -1.000000000000000000, -0.000000000000000000 ) ) ;
#16389=CARTESIAN_POINT ( 'NONE',  ( -34.99999999999998579, 0.000000000000000000, 21.00000000000000355 ) ) ;
#16390=CARTESIAN_POINT ( 'NONE',  ( -36.99999999999997868, 0.000000000000000000, -19.99999999999999289 ) ) ;
#16391=CARTESIAN_POINT ( 'NONE',  ( 37.00000000000003553, 0.000000000000000000, 23.00000000000000355 ) ) ;
#16411=LINE ( 'NONE', #14359, #18762 ) ;
#16415=EDGE_LOOP ( 'NONE', ( #1717, #2234, #19619, #14417 ) ) ;
#16422=DIRECTION ( 'NONE',  ( 0.000000000000000000, 0.000000000000000000, 1.000000000000000000 ) ) ;
#16432=ORIENTED_EDGE ( 'NONE', *, *, #7894, .F. ) ;
#16461=VERTEX_POINT ( 'NONE', #9854 ) ;
#16531=CARTESIAN_POINT ( 'NONE',  ( 35.00000000000003553, -20.00000000000000000, -20.99999999999999645 ) ) ;
#16537=ORIENTED_EDGE ( 'NONE', *, *, #7724, .F. ) ;
#16542=CYLINDRICAL_SURFACE ( 'NONE', #8224, 2.500000000000002220 ) ;
#16549=ORIENTED_EDGE ( 'NONE', *, *, #1932, .T. ) ;
#16550=CARTESIAN_POINT ( 'NONE',  ( 30.99999999999995737, 0.000000000000000000, 31.00000000000000000 ) ) ;
#16569=AXIS2_PLACEMENT_3D ( 'NONE', #15755, #18712, #18916 ) ;
#16589=DIRECTION ( 'NONE',  ( 0.000000000000000000, 0.000000000000000000, -1.000000000000000000 ) ) ;
#16603=DIRECTION ( 'NONE',  ( 1.000000000000000000, 0.000000000000000000, 0.000000000000000000 ) ) ;
#16604=DIRECTION ( 'NONE',  ( 0.000000000000000000, 0.000000000000000000, 1.000000000000000000 ) ) ;
#16608=DIRECTION ( 'NONE',  ( -0.000000000000000000, -1.000000000000000000, -0.000000000000000000 ) ) ;
#16630=CARTESIAN_POINT ( 'NONE',  ( -26.00000000000002842, 3.000000000000000000, 34.00000000000000711 ) ) ;
#16637=DIRECTION ( 'NONE',  ( -0.000000000000000000, -0.000000000000000000, 1.000000000000000000 ) ) ;
#16651=ORIENTED_EDGE ( 'NONE', *, *, #15034, .F. ) ;
#16652=AXIS2_PLACEMENT_3D ( 'NONE', #15754, #4396, #3259 ) ;
#16657=VERTEX_POINT ( 'NONE', #7823 ) ;
#16660=CIRCLE ( 'NONE', #14345, 3.000000000000002665 ) ;
#16676=ADVANCED_FACE ( 'NONE', ( #12367 ), #17191, .F. ) ;
#16684=LINE ( 'NONE', #18493, #14881 ) ;
#16689=EDGE_CURVE ( 'NONE', #7052, #6682, #1620, .T. ) ;
#16710=CARTESIAN_POINT ( 'NONE',  ( -26.00000000000002842, 3.000000000000000000, -39.99999999999999289 ) ) ;
#16716=CARTESIAN_POINT ( 'NONE',  ( 20.99999999999996092, 3.000000000000000000, 32.50000000000000711 ) ) ;
#16749=ORIENTED_EDGE ( 'NONE', *, *, #12799, .T. ) ;
#16766=ORIENTED_EDGE ( 'NONE', *, *, #1221, .F. ) ;
#16779=DIRECTION ( 'NONE',  ( -0.000000000000000000, 1.000000000000000000, -0.000000000000000000 ) ) ;
#16796=FACE_OUTER_BOUND ( 'NONE', #15154, .T. ) ;
#16797=LINE ( 'NONE', #1282, #11354 ) ;
#16813=ORIENTED_EDGE ( 'NONE', *, *, #662, .T. ) ;
#16838=CARTESIAN_POINT ( 'NONE',  ( 22.99999999999995737, 3.000000000000000000, -33.99999999999998579 ) ) ;
#16864=ORIENTED_EDGE ( 'NONE', *, *, #9530, .F. ) ;
#16871=VECTOR ( 'NONE', #6591, 1000.000000000000000 ) ;
#16882=CIRCLE ( 'NONE', #3027, 2.999999999999995559 ) ;
#16883=LINE ( 'NONE', #4211, #3003 ) ;
#16885=DIRECTION ( 'NONE',  ( -1.000000000000000000, -0.000000000000000000, -0.000000000000000000 ) ) ;
#16916=CARTESIAN_POINT ( 'NONE',  ( 0.000000000000000000, 3.000000000000000000, -36.50000000000000000 ) ) ;
#16927=PLANE ( 'NONE',  #4361 ) ;
#16932=ADVANCED_FACE ( 'NONE', ( #11070 ), #1656, .F. ) ;
#16935=VECTOR ( 'NONE', #5389, 1000.000000000000000 ) ;
#16938=AXIS2_PLACEMENT_3D ( 'NONE', #12918, #17644, #19180 ) ;
#16946=CARTESIAN_POINT ( 'NONE',  ( -36.99999999999997868, 3.000000000000000000, -22.99999999999999645 ) ) ;
#16967=ORIENTED_EDGE ( 'NONE', *, *, #14433, .T. ) ;
#16985=CARTESIAN_POINT ( 'NONE',  ( 25.99999999999996092, 0.000000000000000000, -31.00000000000003197 ) ) ;
#16991=CARTESIAN_POINT ( 'NONE',  ( -39.99999999999997868, 3.000000000000000000, -25.99999999999999645 ) ) ;
#17003=EDGE_LOOP ( 'NONE', ( #15715, #19287 ) ) ;
#17033=DIRECTION ( 'NONE',  ( 0.000000000000000000, 0.000000000000000000, 1.000000000000000000 ) ) ;
#17065=ADVANCED_FACE ( 'NONE', ( #17543 ), #11375, .F. ) ;
#17072=DIRECTION ( 'NONE',  ( 0.000000000000000000, 0.000000000000000000, -1.000000000000000000 ) ) ;
#17083=VECTOR ( 'NONE', #4166, 1000.000000000000000 ) ;
#17184=CARTESIAN_POINT ( 'NONE',  ( 30.99999999999999645, 3.000000000000000000, 26.00000000000000355 ) ) ;
#17191=CYLINDRICAL_SURFACE ( 'NONE', #5298, 2.500000000000002220 ) ;
#17196=VECTOR ( 'NONE', #16291, 1000.000000000000000 ) ;
#17224=ADVANCED_FACE ( 'NONE', ( #15877 ), #11118, .T. ) ;
#17312=ORIENTED_EDGE ( 'NONE', *, *, #19850, .T. ) ;
#17323=PRODUCT ( 'Servo-Bas', 'Servo-Bas', '', ( #10762 ) ) ;
#17327=AXIS2_PLACEMENT_3D ( 'NONE', #2660, #7425, #10806 ) ;
#17368=PLANE ( 'NONE',  #14001 ) ;
#17386=ADVANCED_FACE ( 'NONE', ( #5346 ), #12993, .F. ) ;
#17392=FACE_OUTER_BOUND ( 'NONE', #422, .T. ) ;
#17407=DIRECTION ( 'NONE',  ( 0.000000000000000000, -1.000000000000000000, 0.000000000000000000 ) ) ;
#17422=VECTOR ( 'NONE', #1267, 1000.000000000000000 ) ;
#17443=ORIENTED_EDGE ( 'NONE', *, *, #6247, .T. ) ;
#17445=EDGE_LOOP ( 'NONE', ( #1565, #14089, #14936, #5381 ) ) ;
#17467=CARTESIAN_POINT ( 'NONE',  ( 25.99999999999996092, 3.000000000000000000, 40.00000000000000711 ) ) ;
#17473=VECTOR ( 'NONE', #15375, 1000.000000000000000 ) ;
#17479=ORIENTED_EDGE ( 'NONE', *, *, #9130, .T. ) ;
#17485=PLANE ( 'NONE',  #7837 ) ;
#17487=DIRECTION ( 'NONE',  ( -0.000000000000000000, -1.000000000000000000, -0.000000000000000000 ) ) ;
#17492=EDGE_CURVE ( 'NONE', #15883, #9757, #696, .T. ) ;
#17503=CARTESIAN_POINT ( 'NONE',  ( 40.00000000000003553, 3.000000000000000000, 26.00000000000000355 ) ) ;
#17505=LINE ( 'NONE', #3412, #13106 ) ;
#17507=VECTOR ( 'NONE', #8113, 1000.000000000000000 ) ;
#17510=CARTESIAN_POINT ( 'NONE',  ( 40.00000000000003553, 0.000000000000000000, -25.99999999999999645 ) ) ;
#17516=PRODUCT_DEFINITION_FORMATION_WITH_SPECIFIED_SOURCE ( 'ANY', '', #17323, .NOT_KNOWN. ) ;
#17520=EDGE_CURVE ( 'NONE', #7477, #12937, #16883, .T. ) ;
#17531=DIRECTION ( 'NONE',  ( -0.000000000000000000, -1.000000000000000000, -0.000000000000000000 ) ) ;
#17537=LINE ( 'NONE', #17849, #18099 ) ;
#17538=CARTESIAN_POINT ( 'NONE',  ( 22.99999999999995737, 3.000000000000000000, -36.99999999999999289 ) ) ;
#17543=FACE_OUTER_BOUND ( 'NONE', #869, .T. ) ;
#17548=VERTEX_POINT ( 'NONE', #11192 ) ;
#17588=AXIS2_PLACEMENT_3D ( 'NONE', #179, #14399, #6376 ) ;
#17590=CARTESIAN_POINT ( 'NONE',  ( 20.99999999999996092, -20.00000000000000000, 35.00000000000000711 ) ) ;
#17595=LINE ( 'NONE', #8329, #389 ) ;
#17604=VECTOR ( 'NONE', #20069, 1000.000000000000000 ) ;
#17612=CARTESIAN_POINT ( 'NONE',  ( -23.00000000000003197, 0.000000000000000000, 34.00000000000000711 ) ) ;
#17625=DIRECTION ( 'NONE',  ( 0.000000000000000000, 1.000000000000000000, 0.000000000000000000 ) ) ;
#17631=DIRECTION ( 'NONE',  ( -0.000000000000000000, -1.000000000000000000, -0.000000000000000000 ) ) ;
#17644=DIRECTION ( 'NONE',  ( -0.000000000000000000, -1.000000000000000000, -0.000000000000000000 ) ) ;
#17657=ORIENTED_EDGE ( 'NONE', *, *, #18645, .T. ) ;
#17699=DIRECTION ( 'NONE',  ( -0.000000000000000000, -1.000000000000000000, -0.000000000000000000 ) ) ;
#17708=VECTOR ( 'NONE', #15539, 1000.000000000000000 ) ;
#17725=PLANE ( 'NONE',  #8470 ) ;
#17739=ORIENTED_EDGE ( 'NONE', *, *, #19357, .F. ) ;
#17753=ORIENTED_EDGE ( 'NONE', *, *, #4766, .T. ) ;
#17754=DIRECTION ( 'NONE',  ( 0.000000000000000000, 0.000000000000000000, 1.000000000000000000 ) ) ;
#17755=DIRECTION ( 'NONE',  ( -0.000000000000000000, 1.000000000000000000, -0.000000000000000000 ) ) ;
#17789=CARTESIAN_POINT ( 'NONE',  ( -21.00000000000002842, 3.000000000000000000, -37.50000000000000000 ) ) ;
#17794=VERTEX_POINT ( 'NONE', #15413 ) ;
#17809=ORIENTED_EDGE ( 'NONE', *, *, #11697, .T. ) ;
#17849=CARTESIAN_POINT ( 'NONE',  ( 20.99999999999996092, -20.00000000000000000, 32.50000000000000711 ) ) ;
#17858=ORIENTED_EDGE ( 'NONE', *, *, #92, .T. ) ;
#17896=CARTESIAN_POINT ( 'NONE',  ( 40.00000000000003553, -20.00000000000000000, 20.00000000000000355 ) ) ;
#17904=DIRECTION ( 'NONE',  ( -1.000000000000000000, -0.000000000000000000, -0.000000000000000000 ) ) ;
#17933=CARTESIAN_POINT ( 'NONE',  ( -33.99999999999997158, -20.00000000000000000, -22.99999999999999645 ) ) ;
#17937=EDGE_LOOP ( 'NONE', ( #17739, #3728 ) ) ;
#17946=DIRECTION ( 'NONE',  ( -1.000000000000000000, 0.000000000000000000, 0.000000000000000000 ) ) ;
#17949=LINE ( 'NONE', #19474, #16935 ) ;
#17951=CARTESIAN_POINT ( 'NONE',  ( 25.99999999999996092, 0.000000000000000000, -31.00000000000003197 ) ) ;
#17959=CARTESIAN_POINT ( 'NONE',  ( 34.00000000000002842, 3.000000000000000000, 26.00000000000000355 ) ) ;
#17998=CARTESIAN_POINT ( 'NONE',  ( 37.00000000000003553, 0.000000000000000000, 20.00000000000000000 ) ) ;
#18016=DIRECTION ( 'NONE',  ( -0.000000000000000000, -1.000000000000000000, -0.000000000000000000 ) ) ;
#18021=CIRCLE ( 'NONE', #13746, 2.500000000000002220 ) ;
#18030=LINE ( 'NONE', #15259, #2135 ) ;
#18035=CARTESIAN_POINT ( 'NONE',  ( -31.00000000000006395, 3.000000000000000000, -25.99999999999999645 ) ) ;
#18053=VECTOR ( 'NONE', #11130, 1000.000000000000000 ) ;
#18054=ADVANCED_FACE ( 'NONE', ( #1169 ), #8927, .F. ) ;
#18071=AXIS2_PLACEMENT_3D ( 'NONE', #3298, #2151, #5063 ) ;
#18073=VERTEX_POINT ( 'NONE', #15222 ) ;
#18096=ORIENTED_EDGE ( 'NONE', *, *, #19539, .F. ) ;
#18098=AXIS2_PLACEMENT_3D ( 'NONE', #19854, #16604, #19749 ) ;
#18099=VECTOR ( 'NONE', #11678, 1000.000000000000000 ) ;
#18104=VERTEX_POINT ( 'NONE', #7398 ) ;
#18111=DIRECTION ( 'NONE',  ( -0.000000000000000000, -0.000000000000000000, 1.000000000000000000 ) ) ;
#18125=VECTOR ( 'NONE', #5060, 1000.000000000000000 ) ;
#18142=AXIS2_PLACEMENT_3D ( 'NONE', #17590, #6982, #9767 ) ;
#18151=EDGE_CURVE ( 'NONE', #16062, #2620, #7649, .T. ) ;
#18152=CARTESIAN_POINT ( 'NONE',  ( 30.99999999999999645, 3.000000000000000000, 26.00000000000000355 ) ) ;
#18173=AXIS2_PLACEMENT_3D ( 'NONE', #19498, #2096, #6554 ) ;
#18185=DIRECTION ( 'NONE',  ( 0.000000000000000000, 1.000000000000000000, 0.000000000000000000 ) ) ;
#18187=ORIENTED_EDGE ( 'NONE', *, *, #662, .F. ) ;
#18189=DIRECTION ( 'NONE',  ( -0.000000000000000000, -0.000000000000000000, 1.000000000000000000 ) ) ;
#18194=AXIS2_PLACEMENT_3D ( 'NONE', #6827, #13116, #19359 ) ;
#18220=EDGE_CURVE ( 'NONE', #13534, #9868, #6163, .T. ) ;
#18242=EDGE_CURVE ( 'NONE', #11435, #15883, #6970, .T. ) ;
#18251=VECTOR ( 'NONE', #1333, 1000.000000000000000 ) ;
#18253=DIRECTION ( 'NONE',  ( 1.000000000000000000, 0.000000000000000000, 0.000000000000000000 ) ) ;
#18254=CARTESIAN_POINT ( 'NONE',  ( -26.00000000000002842, 3.000000000000000000, -39.99999999999999289 ) ) ;
#18259=CARTESIAN_POINT ( 'NONE',  ( 30.99999999999999645, 0.000000000000000000, 26.00000000000000355 ) ) ;
#18290=ORIENTED_EDGE ( 'NONE', *, *, #14822, .F. ) ;
#18305=CARTESIAN_POINT ( 'NONE',  ( 30.99999999999997158, 0.000000000000000000, 19.99999999999999289 ) ) ;
#18308=VECTOR ( 'NONE', #5144, 1000.000000000000000 ) ;
#18310=DIRECTION ( 'NONE',  ( 0.000000000000000000, 0.000000000000000000, -1.000000000000000000 ) ) ;
#18317=ORIENTED_EDGE ( 'NONE', *, *, #14713, .F. ) ;
#18318=ORIENTED_EDGE ( 'NONE', *, *, #5419, .F. ) ;
#18325=CYLINDRICAL_SURFACE ( 'NONE', #17327, 2.500000000000002220 ) ;
#18333=CARTESIAN_POINT ( 'NONE',  ( 35.00000000000003553, 3.000000000000000000, -18.49999999999999645 ) ) ;
#18348=CARTESIAN_POINT ( 'NONE',  ( 35.00000000000003553, 0.000000000000000000, -20.99999999999999645 ) ) ;
#18351=CARTESIAN_POINT ( 'NONE',  ( -33.99999999999997158, -20.00000000000000000, -25.99999999999999645 ) ) ;
#18354=PRESENTATION_STYLE_ASSIGNMENT (( #8983 ) ) ;
#18358=ORIENTED_EDGE ( 'NONE', *, *, #18943, .F. ) ;
#18398=CARTESIAN_POINT ( 'NONE',  ( 20.99999999999996092, -20.00000000000000000, 37.50000000000001421 ) ) ;
#18471=EDGE_LOOP ( 'NONE', ( #1956, #10066, #4746, #17657 ) ) ;
#18493=CARTESIAN_POINT ( 'NONE',  ( -26.00000000000002842, 3.000000000000000000, -31.00000000000003197 ) ) ;
#18496=VECTOR ( 'NONE', #18189, 1000.000000000000000 ) ;
#18501=CYLINDRICAL_SURFACE ( 'NONE', #253, 2.500000000000002220 ) ;
#18509=VERTEX_POINT ( 'NONE', #1261 ) ;
#18520=DIRECTION ( 'NONE',  ( -0.000000000000000000, -1.000000000000000000, -0.000000000000000000 ) ) ;
#18532=EDGE_CURVE ( 'NONE', #11769, #11321, #6164, .T. ) ;
#18534=VERTEX_POINT ( 'NONE', #15223 ) ;
#18554=ADVANCED_FACE ( 'NONE', ( #10684 ), #5942, .F. ) ;
#18584=CYLINDRICAL_SURFACE ( 'NONE', #9699, 4.999999999999997335 ) ;
#18593=EDGE_LOOP ( 'NONE', ( #19765, #14518, #17479, #291 ) ) ;
#18631=VERTEX_POINT ( 'NONE', #16985 ) ;
#18645=EDGE_CURVE ( 'NONE', #6682, #17548, #966, .T. ) ;
#18646=VERTEX_POINT ( 'NONE', #9135 ) ;
#18648=ORIENTED_EDGE ( 'NONE', *, *, #12814, .F. ) ;
#18649=ORIENTED_EDGE ( 'NONE', *, *, #4740, .F. ) ;
#18658=FACE_OUTER_BOUND ( 'NONE', #15688, .T. ) ;
#18672=ORIENTED_EDGE ( 'NONE', *, *, #4766, .F. ) ;
#18689=ORIENTED_EDGE ( 'NONE', *, *, #7765, .T. ) ;
#18705=DIRECTION ( 'NONE',  ( -0.000000000000000000, -1.000000000000000000, 0.000000000000000000 ) ) ;
#18712=DIRECTION ( 'NONE',  ( 0.000000000000000000, -1.000000000000000000, 0.000000000000000000 ) ) ;
#18741=ORIENTED_EDGE ( 'NONE', *, *, #8396, .T. ) ;
#18762=VECTOR ( 'NONE', #19654, 1000.000000000000000 ) ;
#18784=EDGE_LOOP ( 'NONE', ( #19925, #10231, #19847, #1025 ) ) ;
#18805=DIRECTION ( 'NONE',  ( 0.000000000000000000, 0.000000000000000000, 1.000000000000000000 ) ) ;
#18824=DIRECTION ( 'NONE',  ( 0.000000000000000000, 0.000000000000000000, 1.000000000000000000 ) ) ;
#18830=VECTOR ( 'NONE', #17904, 1000.000000000000000 ) ;
#18844=VECTOR ( 'NONE', #1863, 1000.000000000000000 ) ;
#18849=PLANE ( 'NONE',  #6692 ) ;
#18907=CARTESIAN_POINT ( 'NONE',  ( 19.99999999999995381, 3.000000000000000000, -36.99999999999999289 ) ) ;
#18913=CARTESIAN_POINT ( 'NONE',  ( 35.00000000000003553, 3.000000000000000000, -20.99999999999999645 ) ) ;
#18916=DIRECTION ( 'NONE',  ( 0.000000000000000000, -0.000000000000000000, -1.000000000000000000 ) ) ;
#18942=DIRECTION ( 'NONE',  ( 0.000000000000000000, 1.000000000000000000, 0.000000000000000000 ) ) ;
#18943=EDGE_CURVE ( 'NONE', #6958, #12894, #3070, .T. ) ;
#18980=DIRECTION ( 'NONE',  ( -0.000000000000000000, -1.000000000000000000, -0.000000000000000000 ) ) ;
#19010=VERTEX_POINT ( 'NONE', #19810 ) ;
#19028=ORIENTED_EDGE ( 'NONE', *, *, #2560, .F. ) ;
#19031=ORIENTED_EDGE ( 'NONE', *, *, #17492, .F. ) ;
#19049=AXIS2_PLACEMENT_3D ( 'NONE', #8157, #8045, #14333 ) ;
#19119=EDGE_LOOP ( 'NONE', ( #20122, #8537, #12735, #1152 ) ) ;
#19154=CARTESIAN_POINT ( 'NONE',  ( -20.00000000000003197, 0.000000000000000000, 40.00000000000000711 ) ) ;
#19156=DIRECTION ( 'NONE',  ( 0.000000000000000000, 0.000000000000000000, -1.000000000000000000 ) ) ;
#19160=CARTESIAN_POINT ( 'NONE',  ( -39.99999999999997868, 3.000000000000000000, 26.00000000000000355 ) ) ;
#19180=DIRECTION ( 'NONE',  ( 0.000000000000000000, 0.000000000000000000, -1.000000000000000000 ) ) ;
#19192=CARTESIAN_POINT ( 'NONE',  ( 25.99999999999996092, 0.000000000000000000, 31.00000000000004263 ) ) ;
#19212=ORIENTED_EDGE ( 'NONE', *, *, #7241, .T. ) ;
#19217=ORIENTED_EDGE ( 'NONE', *, *, #20054, .F. ) ;
#19218=LINE ( 'NONE', #16155, #8728 ) ;
#19256=CARTESIAN_POINT ( 'NONE',  ( 30.99999999999999645, 3.000000000000000000, -25.99999999999999645 ) ) ;
#19261=CARTESIAN_POINT ( 'NONE',  ( 0.000000000000000000, 23.00000000000000000, -34.00000000000000000 ) ) ;
#19272=ORIENTED_EDGE ( 'NONE', *, *, #3781, .F. ) ;
#19285=ORIENTED_EDGE ( 'NONE', *, *, #17492, .T. ) ;
#19287=ORIENTED_EDGE ( 'NONE', *, *, #9848, .F. ) ;
#19314=PLANE ( 'NONE',  #18173 ) ;
#19328=AXIS2_PLACEMENT_3D ( 'NONE', #10000, #14837, #7128 ) ;
#19336=EDGE_CURVE ( 'NONE', #12894, #6958, #10682, .T. ) ;
#19345=AXIS2_PLACEMENT_3D ( 'NONE', #15334, #10784, #20033 ) ;
#19357=EDGE_CURVE ( 'NONE', #11769, #16198, #1782, .T. ) ;
#19359=DIRECTION ( 'NONE',  ( 0.000000000000000000, 0.000000000000000000, -1.000000000000000000 ) ) ;
#19372=ORIENTED_EDGE ( 'NONE', *, *, #4428, .T. ) ;
#19374=DIRECTION ( 'NONE',  ( 0.000000000000000000, 0.000000000000000000, 1.000000000000000000 ) ) ;
#19390=CYLINDRICAL_SURFACE ( 'NONE', #13148, 2.500000000000002220 ) ;
#19438=DIRECTION ( 'NONE',  ( 1.000000000000000000, 0.000000000000000000, 1.156482317317870344E-15 ) ) ;
#19474=CARTESIAN_POINT ( 'NONE',  ( -23.00000000000003197, 0.000000000000000000, 34.00000000000000711 ) ) ;
#19477=LINE ( 'NONE', #2266, #7436 ) ;
#19496=ORIENTED_EDGE ( 'NONE', *, *, #19850, .F. ) ;
#19498=CARTESIAN_POINT ( 'NONE',  ( 25.99999999999996092, 3.000000000000000000, -31.00000000000003197 ) ) ;
#19517=CYLINDRICAL_SURFACE ( 'NONE', #18142, 2.500000000000002220 ) ;
#19520=DIRECTION ( 'NONE',  ( 0.000000000000000000, 1.000000000000000000, 0.000000000000000000 ) ) ;
#19539=EDGE_CURVE ( 'NONE', #11502, #4146, #11347, .T. ) ;
#19540=VECTOR ( 'NONE', #16603, 1000.000000000000000 ) ;
#19554=LINE ( 'NONE', #5466, #11645 ) ;
#19555=LINE ( 'NONE', #16710, #2596 ) ;
#19578=CIRCLE ( 'NONE', #15678, 2.500000000000002220 ) ;
#19593=AXIS2_PLACEMENT_3D ( 'NONE', #448, #8868, #6863 ) ;
#19619=ORIENTED_EDGE ( 'NONE', *, *, #18242, .F. ) ;
#19624=EDGE_LOOP ( 'NONE', ( #20334, #9096, #13476, #7209 ) ) ;
#19635=CARTESIAN_POINT ( 'NONE',  ( -23.00000000000003197, 3.000000000000000000, 34.00000000000000711 ) ) ;
#19637=DIRECTION ( 'NONE',  ( -0.000000000000000000, -1.000000000000000000, -0.000000000000000000 ) ) ;
#19644=CARTESIAN_POINT ( 'NONE',  ( -20.00000000000003197, 3.000000000000000000, 40.00000000000000711 ) ) ;
#19654=DIRECTION ( 'NONE',  ( 0.000000000000000000, 0.000000000000000000, -1.000000000000000000 ) ) ;
#19684=VERTEX_POINT ( 'NONE', #10960 ) ;
#19749=DIRECTION ( 'NONE',  ( 1.000000000000000000, 0.000000000000000000, -0.000000000000000000 ) ) ;
#19765=ORIENTED_EDGE ( 'NONE', *, *, #15648, .T. ) ;
#19810=CARTESIAN_POINT ( 'NONE',  ( 25.99999999999996092, 0.000000000000000000, -33.99999999999998579 ) ) ;
#19847=ORIENTED_EDGE ( 'NONE', *, *, #14433, .F. ) ;
#19850=EDGE_CURVE ( 'NONE', #16198, #11823, #17537, .T. ) ;
#19854=CARTESIAN_POINT ( 'NONE',  ( -39.99999999999997868, 3.000000000000000000, -25.99999999999999645 ) ) ;
#19858=VECTOR ( 'NONE', #4042, 1000.000000000000000 ) ;
#19894=LINE ( 'NONE', #1605, #64 ) ;
#19899=CIRCLE ( 'NONE', #10695, 36.50000000000000000 ) ;
#19925=ORIENTED_EDGE ( 'NONE', *, *, #14713, .T. ) ;
#19926=DIRECTION ( 'NONE',  ( -0.000000000000000000, 1.000000000000000000, -0.000000000000000000 ) ) ;
#19927=ORIENTED_EDGE ( 'NONE', *, *, #92, .F. ) ;
#19961=PLANE ( 'NONE',  #3775 ) ;
#19987=LINE ( 'NONE', #11978, #9047 ) ;
#19988=DIRECTION ( 'NONE',  ( 1.000000000000000000, 0.000000000000000000, 1.156482317317870344E-15 ) ) ;
#19989=FACE_OUTER_BOUND ( 'NONE', #4307, .T. ) ;
#19990=DIRECTION ( 'NONE',  ( 1.000000000000000000, 0.000000000000000000, -0.000000000000000000 ) ) ;
#19995=AXIS2_PLACEMENT_3D ( 'NONE', #14276, #3359, #14384 ) ;
#20007=ORIENTED_EDGE ( 'NONE', *, *, #13431, .T. ) ;
#20033=DIRECTION ( 'NONE',  ( 0.000000000000000000, 0.000000000000000000, -1.000000000000000000 ) ) ;
#20046=ADVANCED_FACE ( 'NONE', ( #1764 ), #9724, .F. ) ;
#20050=EDGE_LOOP ( 'NONE', ( #1225, #17858, #8960, #3161 ) ) ;
#20054=EDGE_CURVE ( 'NONE', #9757, #6404, #16411, .T. ) ;
#20069=DIRECTION ( 'NONE',  ( -1.000000000000000000, -0.000000000000000000, -0.000000000000000000 ) ) ;
#20079=DIRECTION ( 'NONE',  ( -1.000000000000000000, 0.000000000000000000, 0.000000000000000000 ) ) ;
#20080=AXIS2_PLACEMENT_3D ( 'NONE', #8394, #17755, #3443 ) ;
#20090=VECTOR ( 'NONE', #14643, 1000.000000000000000 ) ;
#20092=CARTESIAN_POINT ( 'NONE',  ( -26.00000000000002842, 0.000000000000000000, -31.00000000000003197 ) ) ;
#20098=( NAMED_UNIT ( * ) SI_UNIT ( $, .STERADIAN. ) SOLID_ANGLE_UNIT ( ) );
#20111=DIRECTION ( 'NONE',  ( 0.000000000000000000, 1.000000000000000000, 0.000000000000000000 ) ) ;
#20117=CARTESIAN_POINT ( 'NONE',  ( 0.000000000000000000, 16.00000000000000000, -34.00000000000000000 ) ) ;
#20122=ORIENTED_EDGE ( 'NONE', *, *, #9374, .T. ) ;
#20140=VECTOR ( 'NONE', #2196, 1000.000000000000000 ) ;
#20148=CIRCLE ( 'NONE', #11271, 2.500000000000002220 ) ;
#20160=CARTESIAN_POINT ( 'NONE',  ( -21.00000000000002842, 0.000000000000000000, -34.99999999999999289 ) ) ;
#20172=CARTESIAN_POINT ( 'NONE',  ( -21.00000000000002842, -20.00000000000000000, -34.99999999999999289 ) ) ;
#20177=VECTOR ( 'NONE', #2485, 1000.000000000000000 ) ;
#20187=FACE_OUTER_BOUND ( 'NONE', #1653, .T. ) ;
#20188=AXIS2_PLACEMENT_3D ( 'NONE', #20295, #17407, #8044 ) ;
#20237=EDGE_LOOP ( 'NONE', ( #15039, #907, #19217, #10639 ) ) ;
#20238=ORIENTED_EDGE ( 'NONE', *, *, #9758, .F. ) ;
#20244=VECTOR ( 'NONE', #9632, 1000.000000000000000 ) ;
#20268=ORIENTED_EDGE ( 'NONE', *, *, #1503, .F. ) ;
#20292=CARTESIAN_POINT ( 'NONE',  ( -39.99999999999997868, 0.000000000000000000, -25.99999999999999645 ) ) ;
#20295=CARTESIAN_POINT ( 'NONE',  ( 0.000000000000000000, 0.000000000000000000, 0.000000000000000000 ) ) ;
#20324=CARTESIAN_POINT ( 'NONE',  ( -31.00000000000002842, 3.000000000000000000, 31.00000000000000000 ) ) ;
#20334=ORIENTED_EDGE ( 'NONE', *, *, #2817, .F. ) ;
#20351=FACE_OUTER_BOUND ( 'NONE', #7164, .T. ) ;
ENDSEC;
END-ISO-10303-21;
